ISO-10303-21;
HEADER;
FILE_DESCRIPTION (('STEP AP214'),
    '1' );
FILE_NAME ('Bushing.step',
    '2026-10-06T10:59:17',
    ( '' ),
    ( '' ),
    'SwSTEP 2.0',
    'SolidWorks 2026',
    '' );
FILE_SCHEMA (( 'AUTOMOTIVE_DESIGN' ));
ENDSEC;

DATA;
#6=CARTESIAN_POINT ( 'NONE',  ( -5.044287576081563529, 45.27497882680665242, 92.45433879953097289 ) ) ;
#48=CARTESIAN_POINT ( 'NONE',  ( -3.467962453771610498, 40.50591351489412517, 91.93871379611699979 ) ) ;
#62=CARTESIAN_POINT ( 'NONE',  ( -1.876873622437039701, 39.01745058958429269, 93.96996379782397923 ) ) ;
#93=( LENGTH_UNIT ( ) NAMED_UNIT ( * ) SI_UNIT ( .MILLI., .METRE. ) );
#97=CARTESIAN_POINT ( 'NONE',  ( 5.856396280011940014, 46.10368687828906076, 93.18871379782397923 ) ) ;
#105=AXIS2_PLACEMENT_3D ( 'NONE', #8174, #11698, #19756 ) ;
#116=CARTESIAN_POINT ( 'NONE',  ( -2.244031111076484120, 49.10779090901081645, 92.45433879953095868 ) ) ;
#124=CARTESIAN_POINT ( 'NONE',  ( 4.359773538758245692, 47.36728266200564263, 95.05433879953096721 ) ) ;
#139=DIRECTION ( 'NONE',  ( 5.626130192357176673E-16, 1.831515347669941892E-30, -1.000000000000000000 ) ) ;
#148=CARTESIAN_POINT ( 'NONE',  ( -3.134114116279072437, 48.15229756555780227, 92.87621379611699979 ) ) ;
#149=CARTESIAN_POINT ( 'NONE',  ( -5.616286711741430793, 44.43019146960381960, 93.73558879782397923 ) ) ;
#152=CARTESIAN_POINT ( 'NONE',  ( 3.722852957781953798, 40.32059543431686421, 95.05433879953096721 ) ) ;
#195=CARTESIAN_POINT ( 'NONE',  ( 4.673174852049362116, 39.63213674411673537, 92.95433879782399345 ) ) ;
#212=CARTESIAN_POINT ( 'NONE',  ( 0.5221537403065045213, 39.16218137147969003, 94.60386871425484401 ) ) ;
#233=CYLINDRICAL_SURFACE ( 'NONE', #6902, 4.999999999999997335 ) ;
#237=CARTESIAN_POINT ( 'NONE',  ( -0.3594811632358363429, 49.16218137147969003, 93.07733169107483207 ) ) ;
#246=CARTESIAN_POINT ( 'NONE',  ( 6.660594192354429843, 43.89417127335556046, 93.11058879782397923 ) ) ;
#266=DIRECTION ( 'NONE',  ( -5.626130192357176673E-16, -1.831515347669941892E-30, 1.000000000000000000 ) ) ;
#296=CARTESIAN_POINT ( 'NONE',  ( -3.628867371436363953, 48.69222599884265179, 93.57933879782396502 ) ) ;
#314=CARTESIAN_POINT ( 'NONE',  ( -4.884656273474451638, 44.39824779480852612, 94.28246379611698558 ) ) ;
#351=CARTESIAN_POINT ( 'NONE',  ( -3.467962453771611830, 40.50591351489412517, 93.18871379611699979 ) ) ;
#355=CARTESIAN_POINT ( 'NONE',  ( -1.419351766502866541, 49.49642391118513274, 91.15746379782397923 ) ) ;
#377=ORIENTED_EDGE ( 'NONE', *, *, #20663, .T. ) ;
#389=EDGE_CURVE ( 'NONE', #13884, #12946, #15257, .T. ) ;
#398=ORIENTED_EDGE ( 'NONE', *, *, #13707, .T. ) ;
#406=CARTESIAN_POINT ( 'NONE',  ( -4.812088799398940075, 42.22067586467031930, 93.81371379782397923 ) ) ;
#411=LINE ( 'NONE', #11708, #690 ) ;
#449=CARTESIAN_POINT ( 'NONE',  ( 5.358597061094674707, 45.49318455795749117, 92.47037068152910422 ) ) ;
#457=CARTESIAN_POINT ( 'NONE',  ( -3.377490115303421359, 48.14432429247111145, 95.05433879953098142 ) ) ;
#461=CARTESIAN_POINT ( 'NONE',  ( -4.622577041588897373, 46.56120873422322859, 93.81371379782397923 ) ) ;
#545=EDGE_LOOP ( 'NONE', ( #1618, #377, #11663, #17754 ) ) ;
#546=CARTESIAN_POINT ( 'NONE',  ( 3.357643116058060428, 50.56218137147968861, 95.05433879953096721 ) ) ;
#549=DIRECTION ( 'NONE',  ( -5.626130192357176673E-16, -1.831515347669941892E-30, 1.000000000000000000 ) ) ;
#564=CARTESIAN_POINT ( 'NONE',  ( 5.666884522201894647, 41.76315400873614436, 94.28246379782397923 ) ) ;
#576=CARTESIAN_POINT ( 'NONE',  ( 0.5221537403065006355, 44.16218137147969003, 92.45433879953097289 ) ) ;
#578=CARTESIAN_POINT ( 'NONE',  ( 1.864804668130312537, 39.18816951145882399, 95.05433879953096721 ) ) ;
#603=EDGE_CURVE ( 'NONE', #17868, #14152, #6557, .T. ) ;
#620=CIRCLE ( 'NONE', #2330, 6.999999999999999112 ) ;
#661=CARTESIAN_POINT ( 'NONE',  ( -4.009385194876762704, 46.27527268018315709, 94.51683879953097289 ) ) ;
#664=CARTESIAN_POINT ( 'NONE',  ( 0.5221537403064985261, 44.16218137147969003, 96.05433879953096721 ) ) ;
#678=CARTESIAN_POINT ( 'NONE',  ( 5.666884522201896424, 41.76315400873614436, 91.93871379782397923 ) ) ;
#690=VECTOR ( 'NONE', #7095, 1000.000000000000000 ) ;
#706=PRODUCT_DEFINITION_FORMATION_WITH_SPECIFIED_SOURCE ( 'ANY', '', #19896, .NOT_KNOWN. ) ;
#720=LINE ( 'NONE', #20278, #15623 ) ;
#767=EDGE_LOOP ( 'NONE', ( #8584, #12522, #398, #10507 ) ) ;
#787=CARTESIAN_POINT ( 'NONE',  ( 3.394633603133437205, 39.16678578622979501, 95.40913158822179696 ) ) ;
#799=VERTEX_POINT ( 'NONE', #152 ) ;
#815=CARTESIAN_POINT ( 'NONE',  ( 2.232254456934871456, 39.46371826755015633, 93.73558879953097289 ) ) ;
#827=CARTESIAN_POINT ( 'NONE',  ( -1.187946976321871073, 48.86064447540922373, 91.86058879953097289 ) ) ;
#907=CARTESIAN_POINT ( 'NONE',  ( -4.450561708517716930, 41.89428209290792182, 92.45433879953095868 ) ) ;
#930=CARTESIAN_POINT ( 'NONE',  ( 2.232254456934872788, 39.46371826755015633, 91.23558879953097289 ) ) ;
#942=ORIENTED_EDGE ( 'NONE', *, *, #14551, .F. ) ;
#960=FACE_OUTER_BOUND ( 'NONE', #10254, .T. ) ;
#976=CARTESIAN_POINT ( 'NONE',  ( -4.498303996637021740, 46.81144376258747997, 95.05433879953096721 ) ) ;
#986=CARTESIAN_POINT ( 'NONE',  ( 5.052198367669454626, 48.31320248322254685, 93.26683879782399345 ) ) ;
#1005=CARTESIAN_POINT ( 'NONE',  ( -4.812088799398940075, 42.22067586467031930, 95.06371379782397923 ) ) ;
#1016=CARTESIAN_POINT ( 'NONE',  ( -5.111781840388389675, 44.40467396443471415, 92.45433879953098710 ) ) ;
#1075=CARTESIAN_POINT ( 'NONE',  ( -4.884656273474450749, 44.39824779480852612, 93.03246379611697137 ) ) ;
#1086=VERTEX_POINT ( 'NONE', #13615 ) ;
#1092=CARTESIAN_POINT ( 'NONE',  ( 6.660594192354430731, 43.89417127335556046, 93.26683879782399345 ) ) ;
#1100=CARTESIAN_POINT ( 'NONE',  ( -1.876873622437039257, 39.01745058958429269, 92.71996379782397923 ) ) ;
#1107=CARTESIAN_POINT ( 'NONE',  ( -1.876873622437040590, 39.01745058958429269, 95.37621379782397923 ) ) ;
#1118=CARTESIAN_POINT ( 'NONE',  ( 4.512269934384613990, 47.81844922806527620, 93.81371379611699979 ) ) ;
#1119=CIRCLE ( 'NONE', #10988, 4.200000000000001954 ) ;
#1128=CARTESIAN_POINT ( 'NONE',  ( -5.014338679419717337, 43.53652754521196044, 92.45433879953098710 ) ) ;
#1130=CARTESIAN_POINT ( 'NONE',  ( 6.660594192354429843, 43.89417127335556046, 94.51683879782399345 ) ) ;
#1144=CARTESIAN_POINT ( 'NONE',  ( -4.812088799398940075, 42.22067586467031930, 93.81371379782397923 ) ) ;
#1151=CARTESIAN_POINT ( 'NONE',  ( 0.7582201636353291807, 49.56899138526064519, 91.78246379953097289 ) ) ;
#1194=CARTESIAN_POINT ( 'NONE',  ( -1.876873622437039701, 39.01745058958429269, 94.12621379782397923 ) ) ;
#1201=ORIENTED_EDGE ( 'NONE', *, *, #15742, .F. ) ;
#1217=CARTESIAN_POINT ( 'NONE',  ( 0.7901638384306272078, 50.30062182352762079, 94.67308879782399345 ) ) ;
#1228=CARTESIAN_POINT ( 'NONE',  ( -4.007890887056452911, 40.01116025973682611, 95.29808879782397923 ) ) ;
#1311=CARTESIAN_POINT ( 'NONE',  ( 4.155789158466160593, 39.80095668645486029, 95.60097199408900792 ) ) ;
#1323=CARTESIAN_POINT ( 'NONE',  ( -4.498303996637021740, 46.81144376258747997, 95.05433879953096721 ) ) ;
#1335=CARTESIAN_POINT ( 'NONE',  ( -4.622577041588896485, 46.56120873422322859, 92.56371379782397923 ) ) ;
#1357=CARTESIAN_POINT ( 'NONE',  ( 5.053692675489761754, 42.04909006277621586, 93.89183879953097289 ) ) ;
#1428=DIRECTION ( 'NONE',  ( 1.193617070626243237E-16, 1.000000000000000000, 1.876284981264363171E-30 ) ) ;
#1436=CARTESIAN_POINT ( 'NONE',  ( 1.953869608722836881, 49.18494452436591757, 95.05433879953099563 ) ) ;
#1440=CARTESIAN_POINT ( 'NONE',  ( 0.7582201636353292917, 49.56899138526064519, 91.46996379611699979 ) ) ;
#1450=CARTESIAN_POINT ( 'NONE',  ( 5.928963754087451576, 43.92611494815086814, 92.71996379953098710 ) ) ;
#1455=DIRECTION ( 'NONE',  ( -1.239088197126290817E-16, -1.000000000000000000, 0.000000000000000000 ) ) ;
#1466=CARTESIAN_POINT ( 'NONE',  ( 5.220616844236031007, 45.87228208810806507, 92.79808879953097289 ) ) ;
#1509=DIRECTION ( 'NONE',  ( -1.301042606982606060E-16, -1.000000000000000000, 0.000000000000000000 ) ) ;
#1516=ADVANCED_FACE ( 'NONE', ( #18566, #20149 ), #3978, .T. ) ;
#1531=CARTESIAN_POINT ( 'NONE',  ( -4.901157372041539340, 42.48549306292126460, 95.05433879953096721 ) ) ;
#1539=CARTESIAN_POINT ( 'NONE',  ( 4.101515559893016416, 47.72501102306959808, 95.05433879953095300 ) ) ;
#1543=CARTESIAN_POINT ( 'NONE',  ( 2.921181103050040306, 49.30691215337508737, 91.00121379782397923 ) ) ;
#1544=FACE_OUTER_BOUND ( 'NONE', #5148, .T. ) ;
#1568=CARTESIAN_POINT ( 'NONE',  ( 5.666884522201896424, 41.76315400873614436, 91.78246379782397923 ) ) ;
#1593=CARTESIAN_POINT ( 'NONE',  ( 0.5221537403064983041, 37.76218137147968434, 95.05433879953096721 ) ) ;
#1609=ORIENTED_EDGE ( 'NONE', *, *, #4634, .T. ) ;
#1618=ORIENTED_EDGE ( 'NONE', *, *, #14327, .T. ) ;
#1624=AXIS2_PLACEMENT_3D ( 'NONE', #664, #10587, #10264 ) ;
#1626=ORIENTED_EDGE ( 'NONE', *, *, #1842, .F. ) ;
#1642=DIRECTION ( 'NONE',  ( -5.626130192357176673E-16, -1.831515347669941892E-30, 1.000000000000000000 ) ) ;
#1644=CARTESIAN_POINT ( 'NONE',  ( 3.113867759335670726, 48.58372638270478205, 95.05433879953093879 ) ) ;
#1647=CARTESIAN_POINT ( 'NONE',  ( 2.232254456934872344, 39.46371826755015633, 92.17308879611698558 ) ) ;
#1671=CARTESIAN_POINT ( 'NONE',  ( 2.635245049009968366, 48.69372030666295359, 94.20433879953097289 ) ) ;
#1674=CARTESIAN_POINT ( 'NONE',  ( -2.313335635445065375, 50.56218137147968861, 95.05433879953096721 ) ) ;
#1703=CARTESIAN_POINT ( 'NONE',  ( 2.463659247115866258, 38.82793883177424732, 94.12621379782399345 ) ) ;
#1715=VECTOR ( 'NONE', #15071, 1000.000000000000000 ) ;
#1728=CARTESIAN_POINT ( 'NONE',  ( 4.713600934472623294, 47.15680210796202232, 92.45433879953098710 ) ) ;
#1736=CARTESIAN_POINT ( 'NONE',  ( 5.053692675489761754, 42.04909006277621586, 94.82933879611698558 ) ) ;
#1760=CARTESIAN_POINT ( 'NONE',  ( 5.928963754087451576, 43.92611494815086814, 93.65746379611699979 ) ) ;
#1762=CARTESIAN_POINT ( 'NONE',  ( -5.616286711741428128, 44.43019146960381960, 91.23558879782397923 ) ) ;
#1785=CARTESIAN_POINT ( 'NONE',  ( 4.512269934384613101, 47.81844922806527620, 94.12621379953098710 ) ) ;
#1809=FILL_AREA_STYLE_COLOUR ( '', #9110 ) ;
#1812=CARTESIAN_POINT ( 'NONE',  ( -1.876873622437039701, 39.01745058958429269, 93.96996379782397923 ) ) ;
#1842=EDGE_CURVE ( 'NONE', #10155, #10333, #4039, .T. ) ;
#1860=CARTESIAN_POINT ( 'NONE',  ( 2.635245049009969254, 48.69372030666295359, 92.64183879611699979 ) ) ;
#1897=ORIENTED_EDGE ( 'NONE', *, *, #18926, .F. ) ;
#1938=EDGE_CURVE ( 'NONE', #10995, #17381, #4616, .T. ) ;
#1948=CARTESIAN_POINT ( 'NONE',  ( -4.176309363623030180, 42.45208065485131499, 93.42308879953097289 ) ) ;
#1958=CARTESIAN_POINT ( 'NONE',  ( -4.622577041588895597, 46.56120873422322859, 91.31371379782397923 ) ) ;
#2052=CARTESIAN_POINT ( 'NONE',  ( -4.176309363623031068, 42.45208065485131499, 94.67308879953097289 ) ) ;
#2065=CARTESIAN_POINT ( 'NONE',  ( 0.7901638384306286511, 50.30062182352762079, 92.32933879782399345 ) ) ;
#2087=ORIENTED_EDGE ( 'NONE', *, *, #7762, .F. ) ;
#2110=ADVANCED_FACE ( 'NONE', ( #20995 ), #11042, .T. ) ;
#2147=VECTOR ( 'NONE', #1642, 1000.000000000000000 ) ;
#2172=CARTESIAN_POINT ( 'NONE',  ( -3.628867371436362621, 48.69222599884265179, 91.23558879782397923 ) ) ;
#2183=DIRECTION ( 'NONE',  ( 1.290716872006552287E-16, 1.000000000000000000, 0.000000000000000000 ) ) ;
#2244=CARTESIAN_POINT ( 'NONE',  ( 0.5221537403065015237, 49.16218137147969003, 92.72886871425484401 ) ) ;
#2258=CARTESIAN_POINT ( 'NONE',  ( -3.467962453771612275, 40.50591351489411096, 94.75121379953098710 ) ) ;
#2265=DIRECTION ( 'NONE',  ( 1.193617070626243237E-16, 1.000000000000000000, 1.876284981264363171E-30 ) ) ;
#2266=VERTEX_POINT ( 'NONE', #10041 ) ;
#2270=CARTESIAN_POINT ( 'NONE',  ( -5.616286711741429905, 44.43019146960381960, 92.64183879782400766 ) ) ;
#2278=DIRECTION ( 'NONE',  ( -1.000000000000000000, 1.193617070626243237E-16, -5.626130192357177659E-16 ) ) ;
#2299=CARTESIAN_POINT ( 'NONE',  ( 0.5221537403065077410, 49.16218137147969003, 94.29136871766880290 ) ) ;
#2330=AXIS2_PLACEMENT_3D ( 'NONE', #11746, #18220, #16431 ) ;
#2345=DIRECTION ( 'NONE',  ( 1.193617070626243237E-16, 1.000000000000000000, 1.898669798061574161E-30 ) ) ;
#2364=CARTESIAN_POINT ( 'NONE',  ( 5.856396280011940014, 46.10368687828906076, 93.34496379782399345 ) ) ;
#2383=CARTESIAN_POINT ( 'NONE',  ( -4.812088799398939187, 42.22067586467031930, 92.71996379782397923 ) ) ;
#2478=CARTESIAN_POINT ( 'NONE',  ( -0.5863195729081822627, 39.16218137147969003, 94.87115272619178086 ) ) ;
#2506=CARTESIAN_POINT ( 'NONE',  ( -4.007890887056452023, 40.01116025973682611, 95.14183879782397923 ) ) ;
#2582=CARTESIAN_POINT ( 'NONE',  ( 2.463659247115867146, 38.82793883177424732, 92.87621379782399345 ) ) ;
#2605=CARTESIAN_POINT ( 'NONE',  ( 2.273808892390292602, 39.34717618618597612, 95.05433879953095300 ) ) ;
#2630=CARTESIAN_POINT ( 'NONE',  ( -3.246606053099431843, 48.47200184337508233, 92.45433879953098710 ) ) ;
#2697=ORIENTED_EDGE ( 'NONE', *, *, #10554, .T. ) ;
#2716=CARTESIAN_POINT ( 'NONE',  ( 1.031158208426779410, 39.13855439321538654, 92.45433879953100131 ) ) ;
#2718=CARTESIAN_POINT ( 'NONE',  ( 5.052198367669452850, 48.31320248322254685, 94.67308879782399345 ) ) ;
#2742=CARTESIAN_POINT ( 'NONE',  ( 0.2860873169776717573, 38.75537135769874197, 91.15746379953097289 ) ) ;
#2775=CYLINDRICAL_SURFACE ( 'NONE', #17003, 4.999999999999997335 ) ;
#2785=ORIENTED_EDGE ( 'NONE', *, *, #10699, .F. ) ;
#2823=CARTESIAN_POINT ( 'NONE',  ( -4.862798738283528266, 42.89955397074594146, 92.45433879953101552 ) ) ;
#2825=CARTESIAN_POINT ( 'NONE',  ( -4.812088799398938299, 42.22067586467031930, 91.46996379782397923 ) ) ;
#2834=CARTESIAN_POINT ( 'NONE',  ( 4.512269934384613990, 47.81844922806527620, 92.87621379953098710 ) ) ;
#2916=CARTESIAN_POINT ( 'NONE',  ( 2.463659247115865814, 38.82793883177424732, 95.37621379782397923 ) ) ;
#2923=CARTESIAN_POINT ( 'NONE',  ( -1.960491745668696106, 39.53320219679883962, 92.45433879953097289 ) ) ;
#2925=CARTESIAN_POINT ( 'NONE',  ( 5.052198367669454626, 48.31320248322254685, 92.17308879782397923 ) ) ;
#2933=CARTESIAN_POINT ( 'NONE',  ( 5.053692675489762642, 42.04909006277621586, 92.64183879953097289 ) ) ;
#2945=CARTESIAN_POINT ( 'NONE',  ( 5.053692675489763531, 42.04909006277621586, 91.39183879953097289 ) ) ;
#2954=CARTESIAN_POINT ( 'NONE',  ( 0.5221537403064990812, 44.16218137147969003, 95.05433879953096721 ) ) ;
#2992=ORIENTED_EDGE ( 'NONE', *, *, #13629, .T. ) ;
#3025=CARTESIAN_POINT ( 'NONE',  ( 0.5221537403065006355, 48.36218137147969287, 96.05433879953096721 ) ) ;
#3028=CARTESIAN_POINT ( 'NONE',  ( -5.616286711741430793, 44.43019146960381960, 95.14183879782397923 ) ) ;
#3053=CARTESIAN_POINT ( 'NONE',  ( -3.628867371436362621, 48.69222599884265179, 91.07933879782399345 ) ) ;
#3061=DIRECTION ( 'NONE',  ( 1.000000000000000000, 0.000000000000000000, 0.000000000000000000 ) ) ;
#3107=ORIENTED_EDGE ( 'NONE', *, *, #14826, .T. ) ;
#3142=CARTESIAN_POINT ( 'NONE',  ( -3.628867371436363509, 48.69222599884265179, 92.48558879782397923 ) ) ;
#3165=CARTESIAN_POINT ( 'NONE',  ( 4.512269934384614878, 47.81844922806527620, 92.87621379953098710 ) ) ;
#3186=FILL_AREA_STYLE ('',( #1809 ) ) ;
#3203=ORIENTED_EDGE ( 'NONE', *, *, #1938, .F. ) ;
#3208=CARTESIAN_POINT ( 'NONE',  ( 0.7587367783518825792, 49.63488860465389507, 92.45433879953102974 ) ) ;
#3235=CARTESIAN_POINT ( 'NONE',  ( 2.741139475203663967, 48.81344869881760928, 95.05433879953095300 ) ) ;
#3238=CARTESIAN_POINT ( 'NONE',  ( -4.009385194876763592, 46.27527268018315709, 95.45433879611698558 ) ) ;
#3239=CARTESIAN_POINT ( 'NONE',  ( 6.660594192354429843, 43.89417127335556046, 91.86058879782397923 ) ) ;
#3242=EDGE_CURVE ( 'NONE', #6478, #12946, #16195, .T. ) ;
#3249=CARTESIAN_POINT ( 'NONE',  ( 5.220616844236031007, 45.87228208810806507, 92.79808879953097289 ) ) ;
#3264=CARTESIAN_POINT ( 'NONE',  ( 0.2541436421823717873, 38.02374091943176637, 91.54808879782400766 ) ) ;
#3318=( BOUNDED_CURVE ( )  B_SPLINE_CURVE ( 2, ( #6934, #237, #13439, #6726, #10048, #11847, #1948, #6832, #19911, #11959, #19811 ),
 .UNSPECIFIED., .F., .T. ) 
 B_SPLINE_CURVE_WITH_KNOTS ( ( 3, 2, 2, 2, 2, 3 ),
 ( 0.5173390146554853741, 0.5312500000000000000, 0.5625000000000000000, 0.5937500000000000000, 0.6250000000000000000, 0.6423390146554854852 ),
 .UNSPECIFIED. ) 
 CURVE ( )  GEOMETRIC_REPRESENTATION_ITEM ( )  RATIONAL_B_SPLINE_CURVE ( ( 0.9623977609649205789, 0.9661148573551010532, 1.000000000000000000, 0.9238795325112867385, 1.000000000000000000, 0.9238795325112867385, 1.000000000000000000, 0.9238795325112867385, 1.000000000000000000, 0.9577646751561854632, 0.9623977609649205789 ) ) 
 REPRESENTATION_ITEM ( '' )  );
#3330=EDGE_LOOP ( 'NONE', ( #18872, #11689, #16351, #18546 ) ) ;
#3337=CARTESIAN_POINT ( 'NONE',  ( -1.590937568396969315, 39.63064243629642647, 93.26683879611698558 ) ) ;
#3361=CARTESIAN_POINT ( 'NONE',  ( 4.673174852049363004, 39.63213674411673537, 91.70433879782397923 ) ) ;
#3384=( NAMED_UNIT ( * ) SI_UNIT ( $, .STERADIAN. ) SOLID_ANGLE_UNIT ( ) );
#3444=CARTESIAN_POINT ( 'NONE',  ( -4.176309363623031068, 42.45208065485131499, 94.36058879611698558 ) ) ;
#3446=CARTESIAN_POINT ( 'NONE',  ( -4.007890887056452023, 40.01116025973682611, 93.89183879782397923 ) ) ;
#3463=AXIS2_PLACEMENT_3D ( 'NONE', #13241, #18336, #3753 ) ;
#3497=CARTESIAN_POINT ( 'NONE',  ( 5.052198367669454626, 48.31320248322255395, 93.26683879782399345 ) ) ;
#3552=CARTESIAN_POINT ( 'NONE',  ( -1.187946976321871961, 48.86064447540922373, 92.79808879611698558 ) ) ;
#3554=CARTESIAN_POINT ( 'NONE',  ( -1.419351766502867429, 49.49642391118513274, 92.25121379782397923 ) ) ;
#3565=CARTESIAN_POINT ( 'NONE',  ( 3.357643116058062205, 50.56218137147968861, 92.03489701350649455 ) ) ;
#3596=CARTESIAN_POINT ( 'NONE',  ( -3.628867371436364841, 48.69222599884265179, 94.82933879782399345 ) ) ;
#3636=CARTESIAN_POINT ( 'NONE',  ( 0.5221537403065006355, 44.16218137147969003, 92.45433879953097289 ) ) ;
#3646=CARTESIAN_POINT ( 'NONE',  ( -4.002097339596554448, 47.53156763023002895, 95.05433879953091036 ) ) ;
#3647=EDGE_CURVE ( 'NONE', #14806, #7140, #14084, .T. ) ;
#3650=CARTESIAN_POINT ( 'NONE',  ( -4.009385194876762704, 46.27527268018315709, 94.20433879611698558 ) ) ;
#3651=CARTESIAN_POINT ( 'NONE',  ( 2.921181103050040306, 49.30691215337508737, 91.00121379782397923 ) ) ;
#3674=LINE ( 'NONE', #8589, #1715 ) ;
#3678=CARTESIAN_POINT ( 'NONE',  ( 2.635245049009968366, 48.69372030666295359, 94.20433879953097289 ) ) ;
#3752=CARTESIAN_POINT ( 'NONE',  ( -1.876873622437038369, 39.01745058958429269, 91.62621379782397923 ) ) ;
#3753=DIRECTION ( 'NONE',  ( -1.301042606982606060E-16, -1.000000000000000000, 0.000000000000000000 ) ) ;
#3771=CARTESIAN_POINT ( 'NONE',  ( -3.755573279388496832, 40.62988815434074752, 95.05433879953095300 ) ) ;
#3773=ADVANCED_FACE ( 'NONE', ( #5118 ), #8431, .T. ) ;
#3826=EDGE_LOOP ( 'NONE', ( #9500, #10712, #11359, #17078 ) ) ;
#3855=PLANE ( 'NONE',  #12255 ) ;
#3857=CARTESIAN_POINT ( 'NONE',  ( -4.498303996637021740, 46.81144376258747997, 95.05433879953096721 ) ) ;
#3859=EDGE_CURVE ( 'NONE', #10995, #14152, #10144, .T. ) ;
#3861=CARTESIAN_POINT ( 'NONE',  ( -1.419351766502868761, 49.49642391118513274, 94.75121379782397923 ) ) ;
#3872=DIRECTION ( 'NONE',  ( -5.626130192357176673E-16, -1.831515347669941892E-30, 1.000000000000000000 ) ) ;
#3875=CARTESIAN_POINT ( 'NONE',  ( 0.3607607205289448116, 38.91027021862021940, 95.05433879953098142 ) ) ;
#3900=VERTEX_POINT ( 'NONE', #4164 ) ;
#3932=VERTEX_POINT ( 'NONE', #546 ) ;
#3950=CARTESIAN_POINT ( 'NONE',  ( -3.628867371436363953, 48.69222599884265179, 93.73558879782399345 ) ) ;
#3951=CARTESIAN_POINT ( 'NONE',  ( 0.5221537403065040772, 39.16218137147969003, 94.91636871766883132 ) ) ;
#3961=LINE ( 'NONE', #16950, #14851 ) ;
#3964=CARTESIAN_POINT ( 'NONE',  ( -1.876873622437039701, 39.01745058958429269, 94.12621379782397923 ) ) ;
#3978=PLANE ( 'NONE',  #20676 ) ;
#3988=SHAPE_DEFINITION_REPRESENTATION ( #19556, #9056 ) ;
#4039=CIRCLE ( 'NONE', #14908, 6.999999999999999112 ) ;
#4054=CARTESIAN_POINT ( 'NONE',  ( 5.052198367669454626, 48.31320248322255395, 93.42308879782402187 ) ) ;
#4073=CARTESIAN_POINT ( 'NONE',  ( 2.463659247115866258, 38.82793883177424732, 94.28246379782397923 ) ) ;
#4086=CARTESIAN_POINT ( 'NONE',  ( 3.403907234131700488, 40.01403842974062997, 95.05433879953098142 ) ) ;
#4093=CARTESIAN_POINT ( 'NONE',  ( -1.549594827053651924, 39.36475212009352020, 92.45433879953094447 ) ) ;
#4095=FACE_OUTER_BOUND ( 'NONE', #19308, .T. ) ;
#4164=CARTESIAN_POINT ( 'NONE',  ( 0.5221537403064979710, 39.16218137147969003, 93.35386871425482980 ) ) ;
#4196=CARTESIAN_POINT ( 'NONE',  ( -1.987575841473666394, 39.35622280378359505, 95.05433879953096721 ) ) ;
#4231=VERTEX_POINT ( 'NONE', #6 ) ;
#4240=DIRECTION ( 'NONE',  ( -5.626130192357176673E-16, -1.831515347669941892E-30, 1.000000000000000000 ) ) ;
#4262=CARTESIAN_POINT ( 'NONE',  ( -1.876873622437039257, 39.01745058958429269, 92.87621379782399345 ) ) ;
#4270=CARTESIAN_POINT ( 'NONE',  ( -4.812088799398939187, 42.22067586467031930, 92.56371379782397923 ) ) ;
#4299=CARTESIAN_POINT ( 'NONE',  ( -0.9202351150032750393, 39.19788638760600463, 92.45433879953095868 ) ) ;
#4302=CARTESIAN_POINT ( 'NONE',  ( -4.007890887056452023, 40.01116025973682611, 94.04808879782397923 ) ) ;
#4323=EDGE_LOOP ( 'NONE', ( #19592, #5110 ) ) ;
#4326=DIRECTION ( 'NONE',  ( 4.924280921909906060E-16, -1.000000000000000000, -1.532084075168673041E-30 ) ) ;
#4350=FACE_OUTER_BOUND ( 'NONE', #16434, .T. ) ;
#4374=CARTESIAN_POINT ( 'NONE',  ( -4.622577041588896485, 46.56120873422322859, 93.65746379782397923 ) ) ;
#4406=CARTESIAN_POINT ( 'NONE',  ( -4.622577041588895597, 46.56120873422322859, 91.31371379782397923 ) ) ;
#4454=ORIENTED_EDGE ( 'NONE', *, *, #603, .T. ) ;
#4483=CARTESIAN_POINT ( 'NONE',  ( -4.622577041588896485, 46.56120873422322859, 92.40746379782397923 ) ) ;
#4512=CARTESIAN_POINT ( 'NONE',  ( 2.463659247115865369, 38.82793883177424732, 95.53246379782397923 ) ) ;
#4577=CARTESIAN_POINT ( 'NONE',  ( 0.5221537403065079630, 49.16218137147969003, 93.97886871425482980 ) ) ;
#4578=CARTESIAN_POINT ( 'NONE',  ( -1.211118738164628672, 49.47529140343971221, 92.45433879953100131 ) ) ;
#4610=CARTESIAN_POINT ( 'NONE',  ( 5.666884522201894647, 41.76315400873614436, 94.43871379782397923 ) ) ;
#4616=( BOUNDED_CURVE ( )  B_SPLINE_CURVE ( 2, ( #8203, #4993, #6592, #14791, #17878, #314, #16501, #6379, #4780, #9808, #212 ),
 .UNSPECIFIED., .F., .F. ) 
 B_SPLINE_CURVE_WITH_KNOTS ( ( 3, 2, 2, 2, 2, 3 ),
 ( 0.5173390146554853741, 0.5312500000000000000, 0.5625000000000000000, 0.5937500000000000000, 0.6250000000000000000, 0.6423390146554854852 ),
 .UNSPECIFIED. ) 
 CURVE ( )  GEOMETRIC_REPRESENTATION_ITEM ( )  RATIONAL_B_SPLINE_CURVE ( ( 0.9623977609649205789, 0.9661148573551010532, 1.000000000000000000, 0.9238795325112867385, 1.000000000000000000, 0.9238795325112867385, 1.000000000000000000, 0.9238795325112867385, 1.000000000000000000, 0.9577646751561854632, 0.9623977609649205789 ) ) 
 REPRESENTATION_ITEM ( '' )  );
#4632=CARTESIAN_POINT ( 'NONE',  ( -3.467962453771612275, 40.50591351489412517, 94.75121379953098710 ) ) ;
#4634=EDGE_CURVE ( 'NONE', #3932, #11013, #15061, .T. ) ;
#4686=CARTESIAN_POINT ( 'NONE',  ( 4.178421596892070156, 40.17206517740157778, 94.75121379611698558 ) ) ;
#4698=CARTESIAN_POINT ( 'NONE',  ( 3.357643116058058208, 37.76218137147968434, 96.05433879953096721 ) ) ;
#4710=CARTESIAN_POINT ( 'NONE',  ( 0.7901638384306293172, 50.30062182352762079, 91.07933879782399345 ) ) ;
#4711=CARTESIAN_POINT ( 'NONE',  ( 0.7901638384306286511, 50.30062182352762079, 92.17308879782397923 ) ) ;
#4733=CARTESIAN_POINT ( 'NONE',  ( 0.7901638384306293172, 50.30062182352762079, 90.92308879782397923 ) ) ;
#4770=EDGE_LOOP ( 'NONE', ( #19229, #942 ) ) ;
#4780=CARTESIAN_POINT ( 'NONE',  ( -1.590937568396970203, 39.63064243629642647, 94.51683879611698558 ) ) ;
#4783=CARTESIAN_POINT ( 'NONE',  ( 5.434012744193106315, 45.09686908721048582, 92.45433879953098710 ) ) ;
#4800=AXIS2_PLACEMENT_3D ( 'NONE', #6517, #19187, #8019 ) ;
#4822=CARTESIAN_POINT ( 'NONE',  ( 5.053692675489762642, 42.04909006277621586, 93.57933879611698558 ) ) ;
#4823=CARTESIAN_POINT ( 'NONE',  ( 5.856396280011940014, 46.10368687828906076, 93.18871379782397923 ) ) ;
#4847=CARTESIAN_POINT ( 'NONE',  ( 5.928963754087452465, 43.92611494815086814, 92.71996379953098710 ) ) ;
#4869=CARTESIAN_POINT ( 'NONE',  ( 5.666884522201894647, 41.76315400873614436, 94.28246379782397923 ) ) ;
#4918=CARTESIAN_POINT ( 'NONE',  ( -2.294692865963147810, 48.87505292694043391, 95.05433879953096721 ) ) ;
#4921=CARTESIAN_POINT ( 'NONE',  ( -3.467962453771613607, 40.50591351489412517, 95.68871379611699979 ) ) ;
#4923=( BOUNDED_CURVE ( )  B_SPLINE_CURVE ( 2, ( #9943, #449, #10044, #6931, #5331, #11843, #16428 ),
 .UNSPECIFIED., .F., .T. ) 
 B_SPLINE_CURVE_WITH_KNOTS ( ( 3, 2, 2, 3 ),
 ( 0.2122652878748581273, 0.2187500000000000000, 0.2500000000000000000, 0.2673390146554854296 ),
 .UNSPECIFIED. ) 
 CURVE ( )  GEOMETRIC_REPRESENTATION_ITEM ( )  RATIONAL_B_SPLINE_CURVE ( ( 0.9749639689766236295, 0.9842041818081431748, 1.000000000000000000, 0.9238795325112867385, 1.000000000000000000, 0.9577646751561855742, 0.9623977609649205789 ) ) 
 REPRESENTATION_ITEM ( '' )  );
#4948=CARTESIAN_POINT ( 'NONE',  ( 5.220616844236030119, 45.87228208810806507, 94.04808879953097289 ) ) ;
#4993=CARTESIAN_POINT ( 'NONE',  ( -0.3594811632358368425, 49.16218137147969003, 94.01483168766085896 ) ) ;
#4996=CARTESIAN_POINT ( 'NONE',  ( -0.5613265744751935182, 49.60399982207104586, 92.45433879953098710 ) ) ;
#5028=CARTESIAN_POINT ( 'NONE',  ( 2.232254456934871012, 39.46371826755015633, 94.67308879611699979 ) ) ;
#5030=CARTESIAN_POINT ( 'NONE',  ( -4.622577041588896485, 46.56120873422322859, 93.65746379782397923 ) ) ;
#5043=ORIENTED_EDGE ( 'NONE', *, *, #13629, .F. ) ;
#5054=CARTESIAN_POINT ( 'NONE',  ( -4.176309363623031068, 42.45208065485131499, 94.67308879953097289 ) ) ;
#5084=CARTESIAN_POINT ( 'NONE',  ( 2.463659247115867146, 38.82793883177424732, 92.87621379782399345 ) ) ;
#5110=ORIENTED_EDGE ( 'NONE', *, *, #9388, .T. ) ;
#5118=FACE_OUTER_BOUND ( 'NONE', #18194, .T. ) ;
#5134=CARTESIAN_POINT ( 'NONE',  ( 5.220616844236031007, 45.87228208810806507, 93.73558879611698558 ) ) ;
#5136=CARTESIAN_POINT ( 'NONE',  ( 0.2541436421823703995, 38.02374091943176637, 94.04808879782397923 ) ) ;
#5148=EDGE_LOOP ( 'NONE', ( #1201, #7062, #11274, #20752 ) ) ;
#5200=DIRECTION ( 'NONE',  ( 5.626130192357176673E-16, 1.831515347669941892E-30, -1.000000000000000000 ) ) ;
#5240=CARTESIAN_POINT ( 'NONE',  ( 0.2860873169776713132, 38.75537135769874197, 92.09496379611698558 ) ) ;
#5241=CARTESIAN_POINT ( 'NONE',  ( -1.419351766502867429, 49.49642391118513274, 92.40746379782397923 ) ) ;
#5278=EDGE_LOOP ( 'NONE', ( #18270, #1609, #12501, #11463 ) ) ;
#5306=ORIENTED_EDGE ( 'NONE', *, *, #8625, .T. ) ;
#5322=CARTESIAN_POINT ( 'NONE',  ( -2.627048034785010699, 48.88511640015991588, 92.45433879952862810 ) ) ;
#5331=CARTESIAN_POINT ( 'NONE',  ( 2.635245049009969254, 48.69372030666295359, 92.64183879611699979 ) ) ;
#5339=CARTESIAN_POINT ( 'NONE',  ( -3.034344139812558794, 48.41735725404262070, 95.05433879953095300 ) ) ;
#5345=CARTESIAN_POINT ( 'NONE',  ( -4.007890887056452023, 40.01116025973682611, 95.14183879782397923 ) ) ;
#5360=CARTESIAN_POINT ( 'NONE',  ( -2.754305542028548714, 39.77410375191711722, 95.05433879953098142 ) ) ;
#5433=VECTOR ( 'NONE', #3872, 1000.000000000000000 ) ;
#5456=CARTESIAN_POINT ( 'NONE',  ( 5.176818351154000020, 40.65164613849449182, 95.49246367200940711 ) ) ;
#5495=B_SPLINE_CURVE_WITH_KNOTS ( 'NONE', 3,
 ( #9532, #1539, #9839, #16015, #1644, #3235, #16328, #1436, #19504, #7922, #14510, #20978, #14409, #6309, #9737, #8126, #13029, #4918, #11439, #5339, #457, #16744, #3646, #6837, #3857 ),
 .UNSPECIFIED., .F., .F.,
 ( 4, 2, 2, 2, 2, 2, 2, 2, 2, 1, 2, 2, 4 ),
 ( 1.624908565367659545E-10, 0.001304848329475893996, 0.001957272412968412423, 0.002609696496460930416, 0.003914544663445968138, 0.004566968746938486999, 0.005219392830431005860, 0.006524240997416045316, 0.007176665080908565045, 0.007829089164401083906, 0.008481513247893604501, 0.009133937331386125097, 0.01043878549837116282 ),
 .UNSPECIFIED. ) ;
#5545=EDGE_CURVE ( 'NONE', #14408, #20491, #720, .T. ) ;
#5568=CARTESIAN_POINT ( 'NONE',  ( -4.622577041588896485, 46.56120873422322859, 92.56371379782397923 ) ) ;
#5612=DIRECTION ( 'NONE',  ( -1.000000000000000000, -4.924280921909906060E-16, -5.626130192357177659E-16 ) ) ;
#5650=CARTESIAN_POINT ( 'NONE',  ( -4.812088799398940075, 42.22067586467031930, 93.96996379782397923 ) ) ;
#5658=ORIENTED_EDGE ( 'NONE', *, *, #8351, .T. ) ;
#5666=CARTESIAN_POINT ( 'NONE',  ( 4.673174852049363004, 39.63213674411673537, 91.86058879782397923 ) ) ;
#5677=CARTESIAN_POINT ( 'NONE',  ( 3.051792653884171536, 39.75632934307087396, 95.05433879953095300 ) ) ;
#5709=CARTESIAN_POINT ( 'NONE',  ( -4.009385194876760927, 46.27527268018315709, 92.01683879953097289 ) ) ;
#5771=ORIENTED_EDGE ( 'NONE', *, *, #20663, .F. ) ;
#5773=CARTESIAN_POINT ( 'NONE',  ( -5.616286711741429905, 44.43019146960381960, 92.48558879782397923 ) ) ;
#5803=CARTESIAN_POINT ( 'NONE',  ( -4.639915919080545237, 42.28775865649100041, 92.45433879953091605 ) ) ;
#5817=LINE ( 'NONE', #18803, #17408 ) ;
#5905=CARTESIAN_POINT ( 'NONE',  ( 5.666884522201894647, 41.76315400873614436, 94.28246379782397923 ) ) ;
#5906=CARTESIAN_POINT ( 'NONE',  ( 0.5221537403064979710, 39.16218137147969003, 93.35386871425482980 ) ) ;
#5914=CARTESIAN_POINT ( 'NONE',  ( -4.921387819424644761, 43.10902840346005149, 92.45433879953098710 ) ) ;
#5916=CARTESIAN_POINT ( 'NONE',  ( 0.7901638384306278740, 50.30062182352762079, 93.57933879782399345 ) ) ;
#5957=CARTESIAN_POINT ( 'NONE',  ( -4.009385194876761815, 46.27527268018315709, 92.95433879611698558 ) ) ;
#5999=CARTESIAN_POINT ( 'NONE',  ( -3.628867371436365730, 48.69222599884265179, 94.82933879782397923 ) ) ;
#6009=CARTESIAN_POINT ( 'NONE',  ( -5.616286711741428128, 44.43019146960381960, 91.39183879782399345 ) ) ;
#6012=ADVANCED_FACE ( 'NONE', ( #7918 ), #19397, .F. ) ;
#6099=CARTESIAN_POINT ( 'NONE',  ( 5.220616844236031007, 45.87228208810806507, 93.73558879611698558 ) ) ;
#6111=CARTESIAN_POINT ( 'NONE',  ( 0.7901638384306286511, 50.30062182352762079, 92.32933879782399345 ) ) ;
#6122=CARTESIAN_POINT ( 'NONE',  ( 4.178421596892071044, 40.17206517740157778, 92.56371379953098710 ) ) ;
#6138=CARTESIAN_POINT ( 'NONE',  ( -4.176309363623029292, 42.45208065485131499, 90.92308879953097289 ) ) ;
#6145=( LENGTH_UNIT ( ) NAMED_UNIT ( * ) SI_UNIT ( .MILLI., .METRE. ) );
#6171=CARTESIAN_POINT ( 'NONE',  ( 3.357643116058060873, 37.76218137147968434, 95.05433879953096721 ) ) ;
#6182=CARTESIAN_POINT ( 'NONE',  ( 1.618771744999037754, 49.47142490715005181, 92.45433879953100131 ) ) ;
#6217=CARTESIAN_POINT ( 'NONE',  ( 3.394636754364005693, 39.16678693318392135, 95.56538169964434815 ) ) ;
#6227=CARTESIAN_POINT ( 'NONE',  ( -4.498303996637021740, 46.81144376258747997, 95.05433879953096721 ) ) ;
#6237=CARTESIAN_POINT ( 'NONE',  ( -5.616286711741428128, 44.43019146960381960, 91.23558879782397923 ) ) ;
#6244=ADVANCED_FACE ( 'NONE', ( #18544, #17161 ), #3855, .T. ) ;
#6260=DIRECTION ( 'NONE',  ( 1.000000000000000000, -1.193617070626243237E-16, 5.626130192357177659E-16 ) ) ;
#6272=ORIENTED_EDGE ( 'NONE', *, *, #8197, .F. ) ;
#6281=CARTESIAN_POINT ( 'NONE',  ( 4.193944868301254125, 47.85951822794249466, 92.45433879953095868 ) ) ;
#6309=CARTESIAN_POINT ( 'NONE',  ( -0.6433819530550480836, 49.43133198673770323, 95.05433879953093879 ) ) ;
#6312=CARTESIAN_POINT ( 'NONE',  ( -5.616286711741429905, 44.43019146960381960, 92.64183879782400766 ) ) ;
#6335=CARTESIAN_POINT ( 'NONE',  ( 2.232254456934871456, 39.46371826755015633, 93.73558879953097289 ) ) ;
#6379=CARTESIAN_POINT ( 'NONE',  ( -3.467962453771612275, 40.50591351489411096, 94.43871379611699979 ) ) ;
#6415=CARTESIAN_POINT ( 'NONE',  ( -1.590937568396970203, 39.63064243629642647, 94.51683879611698558 ) ) ;
#6440=CARTESIAN_POINT ( 'NONE',  ( 0.2860873169776703140, 38.75537135769874197, 93.65746379953097289 ) ) ;
#6469=CARTESIAN_POINT ( 'NONE',  ( 4.673174852049361228, 39.63213674411673537, 94.20433879782399345 ) ) ;
#6476=CARTESIAN_POINT ( 'NONE',  ( 0.5221537403064985261, 44.16218137147969003, 96.05433879953096721 ) ) ;
#6478=VERTEX_POINT ( 'NONE', #9191 ) ;
#6490=CARTESIAN_POINT ( 'NONE',  ( 4.928447940121048809, 46.77256777370082830, 92.45433879953093026 ) ) ;
#6497=CARTESIAN_POINT ( 'NONE',  ( 5.928963754087450688, 43.92611494815086814, 94.90746379611699979 ) ) ;
#6517=CARTESIAN_POINT ( 'NONE',  ( 0.5221537403065006355, 44.16218137147969003, 92.45433879953097289 ) ) ;
#6527=CARTESIAN_POINT ( 'NONE',  ( -4.176309363623031956, 42.45208065485131499, 95.61058879611698558 ) ) ;
#6528=CARTESIAN_POINT ( 'NONE',  ( 2.921181103050040306, 49.30691215337508737, 90.84496379782399345 ) ) ;
#6538=CARTESIAN_POINT ( 'NONE',  ( 1.630627053521187531, 49.16218137147969003, 92.99615272619178086 ) ) ;
#6546=LINE ( 'NONE', #19526, #19285 ) ;
#6557=( BOUNDED_CURVE ( )  B_SPLINE_CURVE ( 2, ( #6869, #13785, #815, #13375, #10409, #11887, #16778, #20055, #3678, #15175, #10512 ),
 .UNSPECIFIED., .F., .F. ) 
 B_SPLINE_CURVE_WITH_KNOTS ( ( 3, 2, 2, 2, 2, 3 ),
 ( 0.6423390146554854852, 0.6562500000000000000, 0.6875000000000000000, 0.7187500000000000000, 0.7500000000000000000, 0.7673390146554853741 ),
 .UNSPECIFIED. ) 
 CURVE ( )  GEOMETRIC_REPRESENTATION_ITEM ( )  RATIONAL_B_SPLINE_CURVE ( ( 0.9623977609649205789, 0.9661148573551012753, 1.000000000000000000, 0.9238795325112867385, 1.000000000000000000, 0.9238795325112867385, 1.000000000000000000, 0.9238795325112867385, 1.000000000000000000, 0.9577646751561856853, 0.9623977609649205789 ) ) 
 REPRESENTATION_ITEM ( '' )  );
#6576=CARTESIAN_POINT ( 'NONE',  ( -5.547796066657372904, 44.57707013197675394, 94.98020409461749125 ) ) ;
#6592=CARTESIAN_POINT ( 'NONE',  ( -1.187946976321872405, 48.86064447540922373, 94.04808879611699979 ) ) ;
#6603=DIRECTION ( 'NONE',  ( 5.626130192357176673E-16, 1.831515347669941892E-30, -1.000000000000000000 ) ) ;
#6630=CARTESIAN_POINT ( 'NONE',  ( -4.009385194876761815, 46.27527268018315709, 92.95433879611698558 ) ) ;
#6631=CARTESIAN_POINT ( 'NONE',  ( -4.622577041588895597, 46.56120873422322859, 91.15746379782397923 ) ) ;
#6646=CARTESIAN_POINT ( 'NONE',  ( 0.2541436421823703995, 38.02374091943176637, 94.04808879782397923 ) ) ;
#6653=ORIENTED_EDGE ( 'NONE', *, *, #10462, .F. ) ;
#6656=CARTESIAN_POINT ( 'NONE',  ( 0.7582201636353284036, 49.56899138526064519, 93.03246379953100131 ) ) ;
#6672=AXIS2_PLACEMENT_3D ( 'NONE', #15675, #9394, #1509 ) ;
#6682=DIRECTION ( 'NONE',  ( 1.239088197126290817E-16, 1.000000000000000000, 0.000000000000000000 ) ) ;
#6709=CARTESIAN_POINT ( 'NONE',  ( 5.220616844236030119, 45.87228208810806507, 94.98558879611698558 ) ) ;
#6726=CARTESIAN_POINT ( 'NONE',  ( -3.134114116279072881, 48.15229756555780227, 93.18871379953097289 ) ) ;
#6734=CARTESIAN_POINT ( 'NONE',  ( 2.635245049009967921, 48.69372030666295359, 95.14183879611698558 ) ) ;
#6735=CARTESIAN_POINT ( 'NONE',  ( -1.419351766502867873, 49.49642391118513274, 93.50121379782397923 ) ) ;
#6788=CARTESIAN_POINT ( 'NONE',  ( 5.052198367669452850, 48.31320248322255395, 94.51683879782399345 ) ) ;
#6824=DIRECTION ( 'NONE',  ( -5.626130192357176673E-16, -1.831515347669941892E-30, 1.000000000000000000 ) ) ;
#6832=CARTESIAN_POINT ( 'NONE',  ( -3.467962453771611830, 40.50591351489411096, 93.50121379953097289 ) ) ;
#6837=CARTESIAN_POINT ( 'NONE',  ( -4.270168849609139450, 47.18848108112605644, 95.05433879953095300 ) ) ;
#6840=CARTESIAN_POINT ( 'NONE',  ( 2.232254456934871456, 39.46371826755015633, 93.42308879611699979 ) ) ;
#6842=CARTESIAN_POINT ( 'NONE',  ( -5.616286711741428128, 44.43019146960381960, 91.39183879782399345 ) ) ;
#6869=CARTESIAN_POINT ( 'NONE',  ( 0.5221537403065048544, 39.16218137147969003, 93.66636871766883132 ) ) ;
#6893=CARTESIAN_POINT ( 'NONE',  ( -4.622577041588896485, 46.56120873422322859, 93.65746379782397923 ) ) ;
#6900=ORIENTED_EDGE ( 'NONE', *, *, #13707, .F. ) ;
#6902=AXIS2_PLACEMENT_3D ( 'NONE', #3636, #549, #10149 ) ;
#6931=CARTESIAN_POINT ( 'NONE',  ( 4.512269934384613990, 47.81844922806527620, 92.56371379611699979 ) ) ;
#6932=CARTESIAN_POINT ( 'NONE',  ( -0.3594811632358371756, 49.16218137147969003, 94.32733169107483207 ) ) ;
#6934=CARTESIAN_POINT ( 'NONE',  ( 0.5221537403065085181, 49.16218137147969003, 93.04136871766880290 ) ) ;
#6942=CARTESIAN_POINT ( 'NONE',  ( 2.463659247115867146, 38.82793883177424732, 93.03246379782397923 ) ) ;
#6955=CARTESIAN_POINT ( 'NONE',  ( -4.043113822512209410, 40.96171489760612161, 95.05433879953098142 ) ) ;
#6976=( BOUNDED_CURVE ( )  B_SPLINE_CURVE ( 2, ( #5906, #9627, #9214, #14090, #15805, #17588, #6099, #1118, #9415, #7707, #18981 ),
 .UNSPECIFIED., .F., .F. ) 
 B_SPLINE_CURVE_WITH_KNOTS ( ( 3, 2, 2, 2, 2, 3 ),
 ( 0.3923390146554854296, 0.4062500000000000000, 0.4375000000000000000, 0.4687500000000000000, 0.5000000000000000000, 0.5173390146554853741 ),
 .UNSPECIFIED. ) 
 CURVE ( )  GEOMETRIC_REPRESENTATION_ITEM ( )  RATIONAL_B_SPLINE_CURVE ( ( 0.9623977609649205789, 0.9661148573551011642, 1.000000000000000000, 0.9238795325112867385, 1.000000000000000000, 0.9238795325112867385, 1.000000000000000000, 0.9238795325112867385, 1.000000000000000000, 0.9577646751561856853, 0.9623977609649205789 ) ) 
 REPRESENTATION_ITEM ( '' )  );
#7047=CARTESIAN_POINT ( 'NONE',  ( 0.7901638384306293172, 50.30062182352762079, 91.07933879782399345 ) ) ;
#7058=DIRECTION ( 'NONE',  ( 5.626130192357176673E-16, 1.831515347669941892E-30, -1.000000000000000000 ) ) ;
#7059=ORIENTED_EDGE ( 'NONE', *, *, #15366, .T. ) ;
#7062=ORIENTED_EDGE ( 'NONE', *, *, #16213, .T. ) ;
#7091=FACE_OUTER_BOUND ( 'NONE', #545, .T. ) ;
#7095=DIRECTION ( 'NONE',  ( -5.626130192357176673E-16, -1.831515347669941892E-30, 1.000000000000000000 ) ) ;
#7140=VERTEX_POINT ( 'NONE', #10752 ) ;
#7157=CARTESIAN_POINT ( 'NONE',  ( 5.052198367669454626, 48.31320248322254685, 92.17308879782397923 ) ) ;
#7208=AXIS2_PLACEMENT_3D ( 'NONE', #16700, #6603, #7213 ) ;
#7213=DIRECTION ( 'NONE',  ( 1.301042606982606060E-16, 1.000000000000000000, 0.000000000000000000 ) ) ;
#7236=CARTESIAN_POINT ( 'NONE',  ( -4.176309363623030180, 42.45208065485131499, 93.11058879611698558 ) ) ;
#7251=CARTESIAN_POINT ( 'NONE',  ( -5.616286711741430793, 44.43019146960381960, 93.89183879782397923 ) ) ;
#7268=CARTESIAN_POINT ( 'NONE',  ( -1.419351766502868317, 49.49642391118513274, 93.65746379782397923 ) ) ;
#7282=CARTESIAN_POINT ( 'NONE',  ( 4.673174852049361228, 39.63213674411673537, 94.20433879782400766 ) ) ;
#7295=PRODUCT_CONTEXT ( 'NONE', #7770, 'mechanical' ) ;
#7373=CARTESIAN_POINT ( 'NONE',  ( 6.660594192354429843, 43.89417127335556046, 94.51683879782399345 ) ) ;
#7385=CARTESIAN_POINT ( 'NONE',  ( -5.616286711741430793, 44.43019146960381960, 94.98558879782399345 ) ) ;
#7405=EDGE_CURVE ( 'NONE', #3900, #17868, #19169, .T. ) ;
#7446=CARTESIAN_POINT ( 'NONE',  ( 3.357643116058062649, 37.76218137147968434, 92.03489701350649455 ) ) ;
#7469=CLOSED_SHELL ( 'NONE', ( #18775, #9662, #20790, #3773, #15194, #2110, #16979, #15050, #16410, #6244, #9879, #12395, #13302, #1516, #6012, #19383, #19861 ) ) ;
#7476=CARTESIAN_POINT ( 'NONE',  ( 0.7901638384306278740, 50.30062182352762079, 93.42308879782399345 ) ) ;
#7509=CARTESIAN_POINT ( 'NONE',  ( -5.044287576081563529, 45.27497882680665242, 92.45433879953097289 ) ) ;
#7563=CARTESIAN_POINT ( 'NONE',  ( -0.5863195729081845942, 39.16218137147968292, 93.30865272277779354 ) ) ;
#7579=CARTESIAN_POINT ( 'NONE',  ( 5.666884522201894647, 41.76315400873614436, 94.43871379782397923 ) ) ;
#7589=CARTESIAN_POINT ( 'NONE',  ( -3.628867371436363953, 48.69222599884265179, 93.57933879782399345 ) ) ;
#7596=CARTESIAN_POINT ( 'NONE',  ( 0.7901638384306272078, 50.30062182352762079, 94.82933879782397923 ) ) ;
#7606=CARTESIAN_POINT ( 'NONE',  ( 6.660594192354429843, 43.89417127335556046, 94.36058879782399345 ) ) ;
#7618=CARTESIAN_POINT ( 'NONE',  ( -1.876873622437038369, 39.01745058958429269, 91.62621379782397923 ) ) ;
#7634=CARTESIAN_POINT ( 'NONE',  ( -5.044287576081563529, 45.27497882680665242, 92.45433879953097289 ) ) ;
#7665=CARTESIAN_POINT ( 'NONE',  ( -3.467962453771611830, 40.50591351489411096, 93.18871379611699979 ) ) ;
#7688=CARTESIAN_POINT ( 'NONE',  ( -4.007890887056451135, 40.01116025973682611, 92.64183879782400766 ) ) ;
#7705=ORIENTED_EDGE ( 'NONE', *, *, #7762, .T. ) ;
#7706=CARTESIAN_POINT ( 'NONE',  ( 0.2541436421823697334, 38.02374091943176637, 95.29808879782397923 ) ) ;
#7707=CARTESIAN_POINT ( 'NONE',  ( 1.630627053521187086, 49.16218137147969003, 93.93365272277780775 ) ) ;
#7717=CARTESIAN_POINT ( 'NONE',  ( 4.673174852049362116, 39.63213674411673537, 93.11058879782397923 ) ) ;
#7747=SHAPE_REPRESENTATION_RELATIONSHIP ( 'NONE' , 'NONE' ,  #9056, #19981 ) ;
#7762=EDGE_CURVE ( 'NONE', #7140, #1086, #8089, .T. ) ;
#7770=APPLICATION_CONTEXT ( 'automotive_design' ) ;
#7808=CARTESIAN_POINT ( 'NONE',  ( -4.845820878285513444, 46.15288543214547445, 95.05433879953095300 ) ) ;
#7823=CARTESIAN_POINT ( 'NONE',  ( 5.856396280011940902, 46.10368687828906076, 92.09496379782399345 ) ) ;
#7849=CARTESIAN_POINT ( 'NONE',  ( 3.052271114939394625, 39.76217992266624890, 95.01850673350041632 ) ) ;
#7850=ORIENTED_EDGE ( 'NONE', *, *, #7405, .T. ) ;
#7916=CARTESIAN_POINT ( 'NONE',  ( 0.5221537403064990812, 44.16218137147969003, 95.05433879953096721 ) ) ;
#7918=FACE_OUTER_BOUND ( 'NONE', #3826, .T. ) ;
#7922=CARTESIAN_POINT ( 'NONE',  ( 0.8855318251337070956, 49.43213155335586606, 95.05433879953096721 ) ) ;
#7925=CARTESIAN_POINT ( 'NONE',  ( -1.187946976321871073, 48.86064447540922373, 91.54808879611698558 ) ) ;
#7926=CARTESIAN_POINT ( 'NONE',  ( -1.419351766502866541, 49.49642391118513274, 91.00121379782397923 ) ) ;
#7936=ORIENTED_EDGE ( 'NONE', *, *, #8042, .T. ) ;
#7951=CARTESIAN_POINT ( 'NONE',  ( 2.921181103050040306, 49.30691215337508737, 90.84496379782399345 ) ) ;
#7957=( NAMED_UNIT ( * ) SI_UNIT ( $, .STERADIAN. ) SOLID_ANGLE_UNIT ( ) );
#8019=DIRECTION ( 'NONE',  ( -1.290716872006552287E-16, -1.000000000000000000, 0.000000000000000000 ) ) ;
#8028=CARTESIAN_POINT ( 'NONE',  ( -3.134114116279072881, 48.15229756555780227, 94.12621379611699979 ) ) ;
#8029=CARTESIAN_POINT ( 'NONE',  ( 5.052198367669454626, 48.31320248322254685, 92.01683879782399345 ) ) ;
#8042=EDGE_CURVE ( 'NONE', #17381, #16609, #6546, .T. ) ;
#8053=CARTESIAN_POINT ( 'NONE',  ( 6.660594192354429843, 43.89417127335556046, 91.86058879782397923 ) ) ;
#8067=FACE_BOUND ( 'NONE', #4323, .T. ) ;
#8088=EDGE_CURVE ( 'NONE', #2266, #799, #17093, .T. ) ;
#8089=CIRCLE ( 'NONE', #13868, 6.999999999999999112 ) ;
#8126=CARTESIAN_POINT ( 'NONE',  ( -1.692449145443465808, 49.14138036605904603, 95.05433879953098142 ) ) ;
#8130=CARTESIAN_POINT ( 'NONE',  ( 0.7582201636353278484, 49.56899138526064519, 93.96996379611699979 ) ) ;
#8136=EDGE_LOOP ( 'NONE', ( #7705, #5771, #1626, #16118 ) ) ;
#8174=CARTESIAN_POINT ( 'NONE',  ( 0.5221537403064985261, 44.16218137147969003, 96.05433879953096721 ) ) ;
#8197=EDGE_CURVE ( 'NONE', #11013, #14806, #620, .T. ) ;
#8203=CARTESIAN_POINT ( 'NONE',  ( 0.5221537403065079630, 49.16218137147969003, 93.97886871425482980 ) ) ;
#8242=CARTESIAN_POINT ( 'NONE',  ( 4.512269934384614878, 47.81844922806527620, 93.81371379611701400 ) ) ;
#8265=CARTESIAN_POINT ( 'NONE',  ( -1.187946976321871961, 48.86064447540922373, 93.11058879953097289 ) ) ;
#8345=CARTESIAN_POINT ( 'NONE',  ( 0.7582201636353270713, 49.56899138526064519, 95.21996379611698558 ) ) ;
#8347=CARTESIAN_POINT ( 'NONE',  ( -4.007890887056448470, 40.01116025973682611, 91.39183879782399345 ) ) ;
#8351=EDGE_CURVE ( 'NONE', #14152, #16609, #12158, .T. ) ;
#8395=CARTESIAN_POINT ( 'NONE',  ( 2.921181103050038974, 49.30691215337508737, 93.34496379782397923 ) ) ;
#8431=CYLINDRICAL_SURFACE ( 'NONE', #14947, 4.999999999999997335 ) ;
#8447=CARTESIAN_POINT ( 'NONE',  ( 4.178421596892070156, 40.17206517740157778, 93.50121379611699979 ) ) ;
#8449=CARTESIAN_POINT ( 'NONE',  ( 5.856396280011939126, 46.10368687828906076, 94.43871379782397923 ) ) ;
#8460=ORIENTED_EDGE ( 'NONE', *, *, #8351, .F. ) ;
#8561=B_SPLINE_CURVE_WITH_KNOTS ( 'NONE', 3,
 ( #18890, #2716, #18990, #14098, #18673, #15708, #4299, #4093, #2923, #12613, #12506, #20367, #17397, #20673, #10621, #15496, #907, #5803, #19099, #2823, #5914, #1128, #18789, #1016, #11028, #7509 ),
 .UNSPECIFIED., .F., .F.,
 ( 4, 2, 2, 2, 2, 2, 2, 2, 2, 2, 2, 2, 4 ),
 ( 0.000000000000000000, 0.001302007803442155895, 0.001953011705163233518, 0.002604015606884310923, 0.003906023410326472239, 0.004557027312047547477, 0.005208031213768623581, 0.006510039017210761045, 0.007161042918931838884, 0.007812046820652916723, 0.008463050722373993695, 0.009114054624095072402, 0.01041606242753722808 ),
 .UNSPECIFIED. ) ;
#8562=CARTESIAN_POINT ( 'NONE',  ( 0.7901638384306278740, 50.30062182352762079, 93.57933879782399345 ) ) ;
#8584=ORIENTED_EDGE ( 'NONE', *, *, #8042, .F. ) ;
#8589=CARTESIAN_POINT ( 'NONE',  ( 3.357643116058059984, 50.56218137147968861, 96.05433879953096721 ) ) ;
#8625=EDGE_CURVE ( 'NONE', #16609, #799, #20839, .T. ) ;
#8671=CARTESIAN_POINT ( 'NONE',  ( -4.007890887056451135, 40.01116025973682611, 92.79808879782397923 ) ) ;
#8684=CARTESIAN_POINT ( 'NONE',  ( 3.722852957781953798, 40.32059543431686421, 95.05433879953096721 ) ) ;
#8743=CARTESIAN_POINT ( 'NONE',  ( -2.313335635445063598, 50.56218137147968861, 92.03489701350649455 ) ) ;
#8751=ORIENTED_EDGE ( 'NONE', *, *, #14814, .T. ) ;
#8771=CARTESIAN_POINT ( 'NONE',  ( -3.628867371436363509, 48.69222599884265179, 92.48558879782397923 ) ) ;
#8776=VERTEX_POINT ( 'NONE', #17374 ) ;
#8868=CARTESIAN_POINT ( 'NONE',  ( 4.673174852049361228, 39.63213674411673537, 94.36058879782399345 ) ) ;
#8883=CARTESIAN_POINT ( 'NONE',  ( 4.155789158466160593, 39.80095668645486029, 95.44472199408899371 ) ) ;
#8899=CARTESIAN_POINT ( 'NONE',  ( -3.117807152840563756, 40.03267073656082431, 95.05433879953105247 ) ) ;
#8950=PLANE ( 'NONE',  #18770 ) ;
#8980=CARTESIAN_POINT ( 'NONE',  ( 5.666884522201895535, 41.76315400873614436, 93.03246379782397923 ) ) ;
#8999=CARTESIAN_POINT ( 'NONE',  ( -1.876873622437040590, 39.01745058958429269, 95.21996379782397923 ) ) ;
#9056=SHAPE_REPRESENTATION ( 'Bushing', ( #18366 ), #17679 ) ;
#9072=CARTESIAN_POINT ( 'NONE',  ( -3.476578273656611984, 48.74765469743772428, 94.98020409461689439 ) ) ;
#9083=CARTESIAN_POINT ( 'NONE',  ( 5.856396280011940014, 46.10368687828906076, 93.18871379782397923 ) ) ;
#9100=CARTESIAN_POINT ( 'NONE',  ( 4.155795601789611382, 39.80096205483764038, 95.44472229536860652 ) ) ;
#9110=COLOUR_RGB ( '', 0.40784314, 0.44705882, 0.49803922) ;
#9130=CARTESIAN_POINT ( 'NONE',  ( -2.627048034785010699, 48.88511640015991588, 92.45433879952862810 ) ) ;
#9148=APPLICATION_CONTEXT ( 'automotive_design' ) ;
#9160=FACE_OUTER_BOUND ( 'NONE', #8136, .T. ) ;
#9180=( BOUNDED_CURVE ( )  B_SPLINE_CURVE ( 2, ( #2244, #15229, #12046, #17237, #5957, #1075, #7236, #7665, #9377, #7563, #14143 ),
 .UNSPECIFIED., .F., .T. ) 
 B_SPLINE_CURVE_WITH_KNOTS ( ( 3, 2, 2, 2, 2, 3 ),
 ( 0.2673390146554854296, 0.2812500000000000000, 0.3125000000000000000, 0.3437500000000000000, 0.3750000000000000000, 0.3923390146554854296 ),
 .UNSPECIFIED. ) 
 CURVE ( )  GEOMETRIC_REPRESENTATION_ITEM ( )  RATIONAL_B_SPLINE_CURVE ( ( 0.9623977609649205789, 0.9661148573551011642, 1.000000000000000000, 0.9238795325112867385, 1.000000000000000000, 0.9238795325112867385, 1.000000000000000000, 0.9238795325112867385, 1.000000000000000000, 0.9577646751561855742, 0.9623977609649205789 ) ) 
 REPRESENTATION_ITEM ( '' )  );
#9182=CARTESIAN_POINT ( 'NONE',  ( 2.921181103050038530, 49.30691215337508737, 93.50121379782399345 ) ) ;
#9191=CARTESIAN_POINT ( 'NONE',  ( 1.456841371642047411, 39.25032235153333460, 92.45433879953097289 ) ) ;
#9197=VECTOR ( 'NONE', #18416, 1000.000000000000000 ) ;
#9214=CARTESIAN_POINT ( 'NONE',  ( 2.232254456934871456, 39.46371826755015633, 93.42308879611699979 ) ) ;
#9225=CARTESIAN_POINT ( 'NONE',  ( 0.7901638384306272078, 50.30062182352762079, 94.82933879782397923 ) ) ;
#9241=CARTESIAN_POINT ( 'NONE',  ( -4.898310004515241900, 46.00518860734035087, 92.45433879953095868 ) ) ;
#9246=CARTESIAN_POINT ( 'NONE',  ( 4.512269934384615766, 47.81844922806527620, 91.62621379953098710 ) ) ;
#9268=VERTEX_POINT ( 'NONE', #10948 ) ;
#9277=CARTESIAN_POINT ( 'NONE',  ( 0.5221537403065006355, 44.16218137147969003, 92.45433879953097289 ) ) ;
#9301=CARTESIAN_POINT ( 'NONE',  ( -1.419351766502867429, 49.49642391118513274, 92.25121379782397923 ) ) ;
#9329=CARTESIAN_POINT ( 'NONE',  ( -4.812088799398939187, 42.22067586467031930, 92.71996379782397923 ) ) ;
#9343=CARTESIAN_POINT ( 'NONE',  ( -4.007890887056452023, 40.01116025973682611, 93.89183879782397923 ) ) ;
#9377=CARTESIAN_POINT ( 'NONE',  ( -1.590937568396969315, 39.63064243629642647, 93.26683879611698558 ) ) ;
#9388=EDGE_CURVE ( 'NONE', #20491, #17689, #17933, .T. ) ;
#9394=DIRECTION ( 'NONE',  ( -5.626130192357176673E-16, -1.831515347669941892E-30, 1.000000000000000000 ) ) ;
#9396=CARTESIAN_POINT ( 'NONE',  ( -0.3436364127516083888, 49.62902198444135138, 92.45433879953095868 ) ) ;
#9407=ORIENTED_EDGE ( 'NONE', *, *, #16213, .F. ) ;
#9415=CARTESIAN_POINT ( 'NONE',  ( 2.635245049009968810, 48.69372030666295359, 93.89183879611699979 ) ) ;
#9425=CARTESIAN_POINT ( 'NONE',  ( -4.622577041588897373, 46.56120873422322859, 93.81371379782397923 ) ) ;
#9441=CARTESIAN_POINT ( 'NONE',  ( 0.5221537403064990812, 44.16218137147969003, 95.05433879953096721 ) ) ;
#9451=CARTESIAN_POINT ( 'NONE',  ( -3.467962453771611830, 40.50591351489412517, 93.50121379953097289 ) ) ;
#9452=EDGE_LOOP ( 'NONE', ( #6272, #12630, #2087, #14602 ) ) ;
#9498=CARTESIAN_POINT ( 'NONE',  ( -0.9947171538446211159, 49.52734785157042552, 92.45433879953102974 ) ) ;
#9500=ORIENTED_EDGE ( 'NONE', *, *, #5545, .F. ) ;
#9505=DIRECTION ( 'NONE',  ( -5.626130192357176673E-16, -1.831515347669941892E-30, 1.000000000000000000 ) ) ;
#9508=CARTESIAN_POINT ( 'NONE',  ( 2.232254456934871012, 39.46371826755015633, 94.67308879611699979 ) ) ;
#9532=CARTESIAN_POINT ( 'NONE',  ( 4.359773538758245692, 47.36728266200564263, 95.05433879953096721 ) ) ;
#9537=CARTESIAN_POINT ( 'NONE',  ( 2.921181103050039418, 49.30691215337508737, 92.25121379782397923 ) ) ;
#9562=CARTESIAN_POINT ( 'NONE',  ( -1.876873622437038369, 39.01745058958429269, 91.46996379782397923 ) ) ;
#9597=CIRCLE ( 'NONE', #7208, 4.999999999999997335 ) ;
#9616=AXIS2_PLACEMENT_3D ( 'NONE', #17001, #4326, #5612 ) ;
#9627=CARTESIAN_POINT ( 'NONE',  ( 1.403788643848838724, 39.16218137147968292, 93.38983168766081633 ) ) ;
#9637=CARTESIAN_POINT ( 'NONE',  ( 3.357643116058062649, 37.76218137147968434, 92.03489701350649455 ) ) ;
#9643=CARTESIAN_POINT ( 'NONE',  ( -1.419351766502868317, 49.49642391118513274, 93.65746379782397923 ) ) ;
#9644=CARTESIAN_POINT ( 'NONE',  ( 0.7901638384306293172, 50.30062182352762079, 90.92308879782397923 ) ) ;
#9662=ADVANCED_FACE ( 'NONE', ( #18955 ), #10792, .T. ) ;
#9667=CARTESIAN_POINT ( 'NONE',  ( 5.052198367669454626, 48.31320248322254685, 92.01683879782399345 ) ) ;
#9691=SURFACE_SIDE_STYLE ('',( #19761 ) ) ;
#9737=CARTESIAN_POINT ( 'NONE',  ( -1.069770211495338019, 49.34613612695786600, 95.05433879953095300 ) ) ;
#9741=CARTESIAN_POINT ( 'NONE',  ( 5.928963754087451576, 43.92611494815086814, 94.90746379611699979 ) ) ;
#9763=CARTESIAN_POINT ( 'NONE',  ( 3.722707913086011011, 40.32076848204647490, 95.05409729707558597 ) ) ;
#9808=CARTESIAN_POINT ( 'NONE',  ( -0.5863195729081820406, 39.16218137147969003, 94.55865272277780775 ) ) ;
#9811=CARTESIAN_POINT ( 'NONE',  ( 5.024485149279870555, 46.57157721280005092, 92.45433879953095868 ) ) ;
#9834=DIRECTION ( 'NONE',  ( 1.239088197126290817E-16, 1.000000000000000000, 0.000000000000000000 ) ) ;
#9839=CARTESIAN_POINT ( 'NONE',  ( 3.802468188742213151, 48.04124512683031156, 95.05433879953092458 ) ) ;
#9843=CARTESIAN_POINT ( 'NONE',  ( -4.009385194876760927, 46.27527268018315709, 91.70433879611698558 ) ) ;
#9844=CARTESIAN_POINT ( 'NONE',  ( 2.921181103050039418, 49.30691215337508737, 92.09496379782399345 ) ) ;
#9871=CARTESIAN_POINT ( 'NONE',  ( -4.884656273474450749, 44.39824779480852612, 93.34496379953097289 ) ) ;
#9879=ADVANCED_FACE ( 'NONE', ( #9160 ), #12552, .T. ) ;
#9904=CARTESIAN_POINT ( 'NONE',  ( -5.616286711741430793, 44.43019146960381960, 93.73558879782399345 ) ) ;
#9943=CARTESIAN_POINT ( 'NONE',  ( 5.434012744193106315, 45.09686908721048582, 92.45433879953098710 ) ) ;
#9958=CARTESIAN_POINT ( 'NONE',  ( 4.512269934384613101, 47.81844922806527620, 95.06371379611701400 ) ) ;
#9959=CARTESIAN_POINT ( 'NONE',  ( -1.876873622437039701, 39.01745058958429269, 93.96996379782397923 ) ) ;
#9971=ORIENTED_EDGE ( 'NONE', *, *, #3859, .F. ) ;
#9980=PRODUCT_DEFINITION_CONTEXT ( 'detailed design', #9148, 'design' ) ;
#9997=( BOUNDED_SURFACE ( )  B_SPLINE_SURFACE ( 1, 2, ( 
 ( #13802, #12528, #14018, #19015, #20279, #18700, #6138, #15516, #17318, #2742, #930, #12329, #2945, #15412, #10950, #9246, #15733, #1151, #827, #17422, #5709, #12216, #12641, #11052, #17524, #14541, #14434, #20905, #19429, #4847, #1466, #3165, #19532, #6656, #8265, #21005, #16354, #9871, #19633, #9451, #18048, #6440, #6335, #11367, #1357, #12838, #4948, #1785, #1671, #19217, #11573, #19317, #13158, #16045, #5054, #4632, #17836, #20810, #13058, #7849, #9763 ),
 ( #7951, #4733, #14334, #3053, #11263, #6237, #11153, #17621, #9562, #3264, #17940, #3361, #1568, #8053, #17734, #9667, #16148, #12949, #9301, #12583, #4483, #5773, #4270, #7688, #1100, #17475, #2582, #12280, #8980, #18760, #9083, #986, #20452, #7476, #13970, #7589, #4374, #13699, #1144, #9343, #62, #6646, #10612, #7282, #5905, #7606, #18664, #19091, #20357, #1217, #17180, #5999, #15486, #7385, #1005, #2506, #8999, #7706, #2916, #13988, #9100 ) ),
 .UNSPECIFIED., .F., .F., .F. ) 
 B_SPLINE_SURFACE_WITH_KNOTS ( ( 2, 2 ),
 ( 3, 2, 2, 2, 2, 2, 2, 2, 2, 2, 2, 2, 2, 2, 2, 2, 2, 2, 2, 2, 2, 2, 2, 2, 2, 2, 2, 2, 2, 2, 3 ),
 ( 0.000000000000000000, 1.000000000000000000 ),
 ( 0.000000000000000000, 0.03125000000000000000, 0.06250000000000000000, 0.09375000000000000000, 0.1250000000000000000, 0.1562500000000000000, 0.1875000000000000000, 0.2187500000000000000, 0.2500000000000000000, 0.2812500000000000000, 0.3125000000000000000, 0.3437500000000000000, 0.3750000000000000000, 0.4062500000000000000, 0.4375000000000000000, 0.4687500000000000000, 0.5000000000000000000, 0.5312500000000000000, 0.5625000000000000000, 0.5937500000000000000, 0.6250000000000000000, 0.6562500000000000000, 0.6875000000000000000, 0.7187500000000000000, 0.7500000000000000000, 0.7812500000000000000, 0.8125000000000000000, 0.8437500000000000000, 0.8750000000000000000, 0.9062500000000000000, 0.9200238733485665010 ),
 .UNSPECIFIED. ) 
 GEOMETRIC_REPRESENTATION_ITEM ( )  RATIONAL_B_SPLINE_SURFACE ( (
 ( 1.000000000000000000, 0.9238795325112867385, 1.000000000000000000, 0.9238795325112867385, 1.000000000000000000, 0.9238795325112867385, 1.000000000000000000, 0.9238795325112867385, 1.000000000000000000, 0.9238795325112867385, 1.000000000000000000, 0.9238795325112867385, 1.000000000000000000, 0.9238795325112867385, 1.000000000000000000, 0.9238795325112867385, 1.000000000000000000, 0.9238795325112867385, 1.000000000000000000, 0.9238795325112867385, 1.000000000000000000, 0.9238795325112867385, 1.000000000000000000, 0.9238795325112867385, 1.000000000000000000, 0.9238795325112867385, 1.000000000000000000, 0.9238795325112867385, 1.000000000000000000, 0.9238795325112867385, 1.000000000000000000, 0.9238795325112867385, 1.000000000000000000, 0.9238795325112867385, 1.000000000000000000, 0.9238795325112867385, 1.000000000000000000, 0.9238795325112867385, 1.000000000000000000, 0.9238795325112867385, 1.000000000000000000, 0.9238795325112867385, 1.000000000000000000, 0.9238795325112867385, 1.000000000000000000, 0.9238795325112867385, 1.000000000000000000, 0.9238795325112867385, 1.000000000000000000, 0.9238795325112867385, 1.000000000000000000, 0.9238795325112867385, 1.000000000000000000, 0.9238795325112867385, 1.000000000000000000, 0.9238795325112867385, 1.000000000000000000, 0.9238795325112867385, 1.000000000000000000, 0.9664488422904572440, 0.9624739659882119991),
 ( 1.000000000000000000, 0.9238795325112867385, 1.000000000000000000, 0.9238795325112867385, 1.000000000000000000, 0.9238795325112867385, 1.000000000000000000, 0.9238795325112867385, 1.000000000000000000, 0.9238795325112867385, 1.000000000000000000, 0.9238795325112867385, 1.000000000000000000, 0.9238795325112867385, 1.000000000000000000, 0.9238795325112867385, 1.000000000000000000, 0.9238795325112867385, 1.000000000000000000, 0.9238795325112867385, 1.000000000000000000, 0.9238795325112867385, 1.000000000000000000, 0.9238795325112867385, 1.000000000000000000, 0.9238795325112867385, 1.000000000000000000, 0.9238795325112867385, 1.000000000000000000, 0.9238795325112867385, 1.000000000000000000, 0.9238795325112867385, 1.000000000000000000, 0.9238795325112867385, 1.000000000000000000, 0.9238795325112867385, 1.000000000000000000, 0.9238795325112867385, 1.000000000000000000, 0.9238795325112867385, 1.000000000000000000, 0.9238795325112867385, 1.000000000000000000, 0.9238795325112867385, 1.000000000000000000, 0.9238795325112867385, 1.000000000000000000, 0.9238795325112867385, 1.000000000000000000, 0.9238795325112867385, 1.000000000000000000, 0.9238795325112867385, 1.000000000000000000, 0.9238795325112867385, 1.000000000000000000, 0.9238795325112867385, 1.000000000000000000, 0.9238795325112867385, 1.000000000000000000, 0.9664488422904572440, 0.9624739659882119991) ) ) 
 REPRESENTATION_ITEM ( '' )  SURFACE ( )  );
#10007=CARTESIAN_POINT ( 'NONE',  ( 5.856396280011939126, 46.10368687828906076, 94.43871379782397923 ) ) ;
#10041=CARTESIAN_POINT ( 'NONE',  ( -4.901157372041539340, 42.48549306292126460, 95.05433879953096721 ) ) ;
#10044=CARTESIAN_POINT ( 'NONE',  ( 5.220616844236031007, 45.87228208810806507, 92.48558879611698558 ) ) ;
#10048=CARTESIAN_POINT ( 'NONE',  ( -4.009385194876761815, 46.27527268018315709, 93.26683879953097289 ) ) ;
#10056=CARTESIAN_POINT ( 'NONE',  ( 2.635245049009968810, 48.69372030666295359, 93.89183879611699979 ) ) ;
#10058=CARTESIAN_POINT ( 'NONE',  ( -1.876873622437038369, 39.01745058958429269, 91.46996379782397923 ) ) ;
#10104=CARTESIAN_POINT ( 'NONE',  ( -4.901157372041539340, 42.48549306292126460, 95.05433879953096721 ) ) ;
#10124=MECHANICAL_DESIGN_GEOMETRIC_PRESENTATION_REPRESENTATION('',(#11146),#19275);
#10144=LINE ( 'NONE', #16625, #16325 ) ;
#10149=DIRECTION ( 'NONE',  ( -1.301042606982606060E-16, -1.000000000000000000, 0.000000000000000000 ) ) ;
#10152=CARTESIAN_POINT ( 'NONE',  ( -4.884656273474451638, 44.39824779480852612, 94.59496379953098710 ) ) ;
#10155=VERTEX_POINT ( 'NONE', #18594 ) ;
#10162=CARTESIAN_POINT ( 'NONE',  ( 5.928963754087452465, 43.92611494815086814, 92.40746379611699979 ) ) ;
#10163=CARTESIAN_POINT ( 'NONE',  ( 5.666884522201895535, 41.76315400873614436, 93.18871379782397923 ) ) ;
#10183=AXIS2_PLACEMENT_3D ( 'NONE', #9441, #15927, #1455 ) ;
#10254=EDGE_LOOP ( 'NONE', ( #19938, #13936, #12551, #2785 ) ) ;
#10264=DIRECTION ( 'NONE',  ( 1.290716872006552287E-16, 1.000000000000000000, 0.000000000000000000 ) ) ;
#10275=CARTESIAN_POINT ( 'NONE',  ( 0.2541436421823717318, 38.02374091943176637, 91.70433879782397923 ) ) ;
#10290=CARTESIAN_POINT ( 'NONE',  ( 1.656782470118943751, 39.12201036244813679, 95.05433879953095300 ) ) ;
#10333=VERTEX_POINT ( 'NONE', #1674 ) ;
#10370=CARTESIAN_POINT ( 'NONE',  ( -3.134114116279072881, 48.15229756555780227, 94.43871379953097289 ) ) ;
#10376=CARTESIAN_POINT ( 'NONE',  ( 0.5221537403064990812, 44.16218137147969003, 95.05433879953096721 ) ) ;
#10384=CARTESIAN_POINT ( 'NONE',  ( 2.463659247115866258, 38.82793883177424732, 94.12621379782399345 ) ) ;
#10409=CARTESIAN_POINT ( 'NONE',  ( 5.053692675489761754, 42.04909006277621586, 93.89183879953097289 ) ) ;
#10462=EDGE_CURVE ( 'NONE', #6478, #4231, #8561, .T. ) ;
#10474=CARTESIAN_POINT ( 'NONE',  ( -4.622577041588896485, 46.56120873422322859, 92.56371379782397923 ) ) ;
#10487=DIRECTION ( 'NONE',  ( -5.626130192357176673E-16, -1.831515347669941892E-30, 1.000000000000000000 ) ) ;
#10490=CARTESIAN_POINT ( 'NONE',  ( 0.2541436421823697334, 38.02374091943176637, 95.29808879782397923 ) ) ;
#10502=CARTESIAN_POINT ( 'NONE',  ( -4.901157372041539340, 42.48549306292126460, 95.05433879953096721 ) ) ;
#10507=ORIENTED_EDGE ( 'NONE', *, *, #8625, .F. ) ;
#10512=CARTESIAN_POINT ( 'NONE',  ( 0.5221537403065076299, 49.16218137147969003, 94.29136871766880290 ) ) ;
#10554=EDGE_CURVE ( 'NONE', #8776, #18462, #5495, .T. ) ;
#10566=DIRECTION ( 'NONE',  ( -5.626130192357176673E-16, -1.831515347669941892E-30, 1.000000000000000000 ) ) ;
#10582=CARTESIAN_POINT ( 'NONE',  ( -4.007890887056452023, 40.01116025973682611, 94.04808879782399345 ) ) ;
#10587=DIRECTION ( 'NONE',  ( 5.626130192357176673E-16, 1.831515347669941892E-30, -1.000000000000000000 ) ) ;
#10600=CARTESIAN_POINT ( 'NONE',  ( 4.673174852049361228, 39.63213674411673537, 94.20433879782400766 ) ) ;
#10612=CARTESIAN_POINT ( 'NONE',  ( 2.463659247115866258, 38.82793883177424732, 94.12621379782399345 ) ) ;
#10621=CARTESIAN_POINT ( 'NONE',  ( -3.988948728167713398, 41.15132427329136533, 92.45433879953091605 ) ) ;
#10650=CIRCLE ( 'NONE', #20458, 4.999999999999997335 ) ;
#10699=EDGE_CURVE ( 'NONE', #10155, #7140, #3961, .T. ) ;
#10712=ORIENTED_EDGE ( 'NONE', *, *, #14551, .T. ) ;
#10722=CARTESIAN_POINT ( 'NONE',  ( -0.2947060777460364656, 38.91366773902584697, 95.05433879953096721 ) ) ;
#10752=CARTESIAN_POINT ( 'NONE',  ( -2.313335635445065375, 37.76218137147968434, 96.05433879953096721 ) ) ;
#10776=AXIS2_PLACEMENT_3D ( 'NONE', #14042, #4240, #11076 ) ;
#10788=CARTESIAN_POINT ( 'NONE',  ( 0.2541436421823710656, 38.02374091943176637, 92.95433879782399345 ) ) ;
#10792=CYLINDRICAL_SURFACE ( 'NONE', #6672, 4.999999999999997335 ) ;
#10802=CARTESIAN_POINT ( 'NONE',  ( 2.921181103050038086, 49.30691215337508737, 94.75121379782399345 ) ) ;
#10829=CARTESIAN_POINT ( 'NONE',  ( 2.463659247115867146, 38.82793883177424732, 93.03246379782397923 ) ) ;
#10894=DIRECTION ( 'NONE',  ( 1.239088197126290817E-16, 1.000000000000000000, 0.000000000000000000 ) ) ;
#10929=CARTESIAN_POINT ( 'NONE',  ( 2.921181103050038086, 49.30691215337508737, 94.75121379782399345 ) ) ;
#10948=CARTESIAN_POINT ( 'NONE',  ( 0.5221537403064990812, 39.96218137147968719, 92.45433879953097289 ) ) ;
#10950=CARTESIAN_POINT ( 'NONE',  ( 5.220616844236031895, 45.87228208810806507, 91.54808879953097289 ) ) ;
#10988=AXIS2_PLACEMENT_3D ( 'NONE', #576, #7058, #2183 ) ;
#10995=VERTEX_POINT ( 'NONE', #4577 ) ;
#11009=CARTESIAN_POINT ( 'NONE',  ( -4.622577041588897373, 46.56120873422322859, 95.06371379782397923 ) ) ;
#11013=VERTEX_POINT ( 'NONE', #12475 ) ;
#11028=CARTESIAN_POINT ( 'NONE',  ( -5.103836094787935984, 44.83927886749827962, 92.45433879953098710 ) ) ;
#11030=CARTESIAN_POINT ( 'NONE',  ( -1.876873622437039701, 39.01745058958429269, 94.12621379782397923 ) ) ;
#11039=CARTESIAN_POINT ( 'NONE',  ( 1.456841371642047411, 39.25032235153333460, 92.45433879953097289 ) ) ;
#11042=CYLINDRICAL_SURFACE ( 'NONE', #10183, 6.999999999999999112 ) ;
#11052=CARTESIAN_POINT ( 'NONE',  ( -3.467962453771610498, 40.50591351489412517, 92.25121379953098710 ) ) ;
#11076=DIRECTION ( 'NONE',  ( -1.239088197126290817E-16, -1.000000000000000000, 0.000000000000000000 ) ) ;
#11109=CARTESIAN_POINT ( 'NONE',  ( 0.5221537403065045213, 39.16218137147969003, 94.60386871425484401 ) ) ;
#11121=DIRECTION ( 'NONE',  ( 5.626130192357176673E-16, 1.809130530872730902E-30, -1.000000000000000000 ) ) ;
#11130=CARTESIAN_POINT ( 'NONE',  ( 5.666884522201895535, 41.76315400873614436, 93.18871379782397923 ) ) ;
#11146=STYLED_ITEM ( 'NONE', ( #17758 ), #11462 ) ;
#11153=CARTESIAN_POINT ( 'NONE',  ( -4.812088799398938299, 42.22067586467031930, 91.31371379782397923 ) ) ;
#11227=FACE_OUTER_BOUND ( 'NONE', #20165, .T. ) ;
#11238=CARTESIAN_POINT ( 'NONE',  ( -4.007890887056448470, 40.01116025973682611, 91.54808879782400766 ) ) ;
#11240=CARTESIAN_POINT ( 'NONE',  ( 0.2541436421823717873, 38.02374091943176637, 91.54808879782400766 ) ) ;
#11263=CARTESIAN_POINT ( 'NONE',  ( -4.622577041588895597, 46.56120873422322859, 91.15746379782397923 ) ) ;
#11274=ORIENTED_EDGE ( 'NONE', *, *, #14826, .F. ) ;
#11298=CARTESIAN_POINT ( 'NONE',  ( 0.5221537403065048544, 39.16218137147969003, 93.66636871766883132 ) ) ;
#11344=CARTESIAN_POINT ( 'NONE',  ( -1.187946976321873294, 48.86064447540922373, 95.29808879611699979 ) ) ;
#11359=ORIENTED_EDGE ( 'NONE', *, *, #20903, .T. ) ;
#11367=CARTESIAN_POINT ( 'NONE',  ( 4.178421596892070156, 40.17206517740157778, 93.81371379953100131 ) ) ;
#11392=CARTESIAN_POINT ( 'NONE',  ( -4.622577041588897373, 46.56120873422322859, 94.90746379782396502 ) ) ;
#11439=CARTESIAN_POINT ( 'NONE',  ( -2.677692965280757953, 48.66802378075904301, 95.05433879953109511 ) ) ;
#11442=CARTESIAN_POINT ( 'NONE',  ( -4.884656273474449861, 44.39824779480852612, 91.78246379611699979 ) ) ;
#11443=CARTESIAN_POINT ( 'NONE',  ( -4.622577041588896485, 46.56120873422322859, 92.40746379782397923 ) ) ;
#11462=MANIFOLD_SOLID_BREP ( 'Stock-MAS-160-1', #7469 ) ;
#11463=ORIENTED_EDGE ( 'NONE', *, *, #15889, .F. ) ;
#11500=DIRECTION ( 'NONE',  ( 5.626130192357176673E-16, 1.831515347669941892E-30, -1.000000000000000000 ) ) ;
#11515=CARTESIAN_POINT ( 'NONE',  ( 0.3123767374396226315, 49.66473798958180197, 92.45433879953097289 ) ) ;
#11529=DIRECTION ( 'NONE',  ( -5.626130192357176673E-16, -1.831515347669941892E-30, 1.000000000000000000 ) ) ;
#11547=CARTESIAN_POINT ( 'NONE',  ( 3.722706642241001784, 40.32076742321550000, 95.99159722619801016 ) ) ;
#11549=CARTESIAN_POINT ( 'NONE',  ( -4.812088799398940075, 42.22067586467031930, 93.81371379782397923 ) ) ;
#11573=CARTESIAN_POINT ( 'NONE',  ( -1.187946976321872850, 48.86064447540922373, 94.36058879953097289 ) ) ;
#11610=VECTOR ( 'NONE', #6260, 1000.000000000000000 ) ;
#11614=( BOUNDED_CURVE ( )  B_SPLINE_CURVE ( 2, ( #19244, #12864, #19344, #14989, #14875, #15098, #5084, #195, #12974, #18078, #97, #3497, #8395, #16484, #19454, #296, #6893, #9904, #406, #13397, #1812, #13083, #1703, #6469, #4869, #18180, #10007, #6788, #13185, #19659, #16587, #3596, #11392, #6576, #10104 ),
 .UNSPECIFIED., .F., .T. ) 
 B_SPLINE_CURVE_WITH_KNOTS ( ( 3, 2, 2, 2, 2, 2, 2, 2, 2, 2, 2, 2, 2, 2, 2, 2, 2, 3 ),
 ( 0.3500748721534128194, 0.3736316088721369777, 0.4075981187696039454, 0.4415646286670709131, 0.4755311385645378808, 0.5094976484620048485, 0.5434641583594719272, 0.5774306682569388949, 0.6113971781544058626, 0.6453636880518728303, 0.6793301979493397980, 0.7132967078468067657, 0.7472632177442737333, 0.7812297276417408121, 0.8151962375392077798, 0.8491627474366747474, 0.8831292573341417151, 0.9149214517709542971 ),
 .UNSPECIFIED. ) 
 CURVE ( )  GEOMETRIC_REPRESENTATION_ITEM ( )  RATIONAL_B_SPLINE_CURVE ( ( 0.9676416783622849849, 0.9472082996766311158, 1.000000000000000000, 0.9238795325112867385, 1.000000000000000000, 0.9238795325112867385, 1.000000000000000000, 0.9238795325112867385, 1.000000000000000000, 0.9238795325112867385, 1.000000000000000000, 0.9238795325112867385, 1.000000000000000000, 0.9238795325112867385, 1.000000000000000000, 0.9238795325112867385, 1.000000000000000000, 0.9238795325112867385, 1.000000000000000000, 0.9238795325112867385, 1.000000000000000000, 0.9238795325112867385, 1.000000000000000000, 0.9238795325112867385, 1.000000000000000000, 0.9238795325112867385, 1.000000000000000000, 0.9238795325112867385, 1.000000000000000000, 0.9238795325112867385, 1.000000000000000000, 0.9238795325112867385, 1.000000000000000000, 0.9287522706828729158, 0.9908783657868658334 ) ) 
 REPRESENTATION_ITEM ( '' )  );
#11642=FACE_OUTER_BOUND ( 'NONE', #20083, .T. ) ;
#11656=CARTESIAN_POINT ( 'NONE',  ( 2.463659247115867590, 38.82793883177424732, 91.62621379782397923 ) ) ;
#11661=CARTESIAN_POINT ( 'NONE',  ( 0.5221537403065045213, 39.16218137147969003, 94.60386871425484401 ) ) ;
#11663=ORIENTED_EDGE ( 'NONE', *, *, #20256, .T. ) ;
#11685=EDGE_LOOP ( 'NONE', ( #19826, #16149, #17855, #5043 ) ) ;
#11689=ORIENTED_EDGE ( 'NONE', *, *, #18796, .T. ) ;
#11698=DIRECTION ( 'NONE',  ( 5.626130192357176673E-16, 1.831515347669941892E-30, -1.000000000000000000 ) ) ;
#11708=CARTESIAN_POINT ( 'NONE',  ( 0.5221537403065000804, 39.96218137147968719, 92.45433879953097289 ) ) ;
#11746=CARTESIAN_POINT ( 'NONE',  ( 0.5221537403064985261, 44.16218137147969003, 96.05433879953096721 ) ) ;
#11756=CARTESIAN_POINT ( 'NONE',  ( 4.512269934384614878, 47.81844922806527620, 92.56371379611699979 ) ) ;
#11757=CARTESIAN_POINT ( 'NONE',  ( -4.812088799398940075, 42.22067586467031930, 95.06371379782397923 ) ) ;
#11837=ORIENTED_EDGE ( 'NONE', *, *, #3859, .T. ) ;
#11843=CARTESIAN_POINT ( 'NONE',  ( 1.630627053521184200, 49.16218137147969003, 92.68365272277780775 ) ) ;
#11847=CARTESIAN_POINT ( 'NONE',  ( -4.884656273474450749, 44.39824779480852612, 93.34496379953098710 ) ) ;
#11857=CARTESIAN_POINT ( 'NONE',  ( 5.856396280011940902, 46.10368687828906076, 92.09496379782399345 ) ) ;
#11887=CARTESIAN_POINT ( 'NONE',  ( 5.928963754087450688, 43.92611494815086814, 93.96996379953098710 ) ) ;
#11953=VERTEX_POINT ( 'NONE', #5322 ) ;
#11959=CARTESIAN_POINT ( 'NONE',  ( -0.5863195729081815966, 39.16218137147969003, 93.62115272619176665 ) ) ;
#11969=CARTESIAN_POINT ( 'NONE',  ( -4.812088799398938299, 42.22067586467031930, 91.46996379782397923 ) ) ;
#11970=FACE_OUTER_BOUND ( 'NONE', #767, .T. ) ;
#12031=ORIENTED_EDGE ( 'NONE', *, *, #15429, .F. ) ;
#12046=CARTESIAN_POINT ( 'NONE',  ( -1.187946976321871961, 48.86064447540922373, 92.79808879611698558 ) ) ;
#12071=CARTESIAN_POINT ( 'NONE',  ( 5.856396280011940014, 46.10368687828906076, 93.34496379782399345 ) ) ;
#12083=CARTESIAN_POINT ( 'NONE',  ( -3.602792415931784120, 40.47352456204527016, 95.05433879953102405 ) ) ;
#12110=VERTEX_POINT ( 'NONE', #6171 ) ;
#12158=( BOUNDED_CURVE ( )  B_SPLINE_CURVE ( 2, ( #15355, #6932, #18641, #10370, #661, #10152, #2052, #2258, #13748, #2478, #3951 ),
 .UNSPECIFIED., .F., .F. ) 
 B_SPLINE_CURVE_WITH_KNOTS ( ( 3, 2, 2, 2, 2, 3 ),
 ( 0.7673390146554853741, 0.7812500000000000000, 0.8125000000000000000, 0.8437500000000000000, 0.8750000000000000000, 0.8923390146554854852 ),
 .UNSPECIFIED. ) 
 CURVE ( )  GEOMETRIC_REPRESENTATION_ITEM ( )  RATIONAL_B_SPLINE_CURVE ( ( 0.9623977609649205789, 0.9661148573551010532, 1.000000000000000000, 0.9238795325112867385, 1.000000000000000000, 0.9238795325112867385, 1.000000000000000000, 0.9238795325112867385, 1.000000000000000000, 0.9577646751561854632, 0.9623977609649205789 ) ) 
 REPRESENTATION_ITEM ( '' )  );
#12159=EDGE_LOOP ( 'NONE', ( #6653, #16490, #18339, #4454, #5658, #5306, #20168, #9407 ) ) ;
#12160=CARTESIAN_POINT ( 'NONE',  ( -3.950384684012687053, 48.00272989695906745, 92.51086634195935687 ) ) ;
#12170=CARTESIAN_POINT ( 'NONE',  ( 0.5221537403065040772, 39.16218137147969003, 94.91636871766883132 ) ) ;
#12176=CARTESIAN_POINT ( 'NONE',  ( -3.628867371436363953, 48.69222599884265179, 93.73558879782397923 ) ) ;
#12216=CARTESIAN_POINT ( 'NONE',  ( -4.884656273474450749, 44.39824779480852612, 92.09496379953097289 ) ) ;
#12255=AXIS2_PLACEMENT_3D ( 'NONE', #10376, #16846, #2265 ) ;
#12269=ORIENTED_EDGE ( 'NONE', *, *, #10462, .T. ) ;
#12270=CARTESIAN_POINT ( 'NONE',  ( -4.812088799398939187, 42.22067586467031930, 92.71996379782397923 ) ) ;
#12280=CARTESIAN_POINT ( 'NONE',  ( 4.673174852049362116, 39.63213674411673537, 92.95433879782399345 ) ) ;
#12282=CARTESIAN_POINT ( 'NONE',  ( 2.232254456934870568, 39.46371826755015633, 94.98558879953097289 ) ) ;
#12288=CARTESIAN_POINT ( 'NONE',  ( -5.616286711741430793, 44.43019146960381960, 95.14183879782397923 ) ) ;
#12301=CARTESIAN_POINT ( 'NONE',  ( -1.582249008360334885, 39.19284116845371813, 95.05433879953098142 ) ) ;
#12329=CARTESIAN_POINT ( 'NONE',  ( 4.178421596892071932, 40.17206517740157778, 91.31371379953098710 ) ) ;
#12375=CARTESIAN_POINT ( 'NONE',  ( -2.627048034785010699, 48.88511640015991588, 92.45433879952862810 ) ) ;
#12389=CARTESIAN_POINT ( 'NONE',  ( -4.007890887056452911, 40.01116025973682611, 95.29808879782397923 ) ) ;
#12395=ADVANCED_FACE ( 'NONE', ( #8067, #21023 ), #12963, .F. ) ;
#12413=CARTESIAN_POINT ( 'NONE',  ( -5.616286711741430793, 44.43019146960381960, 93.89183879782397923 ) ) ;
#12475=CARTESIAN_POINT ( 'NONE',  ( 3.357643116058059984, 50.56218137147968861, 96.05433879953096721 ) ) ;
#12482=CARTESIAN_POINT ( 'NONE',  ( 0.5221537403064999694, 39.16218137147969003, 92.45433879953097289 ) ) ;
#12501=ORIENTED_EDGE ( 'NONE', *, *, #8197, .T. ) ;
#12506=CARTESIAN_POINT ( 'NONE',  ( -2.712716146932703687, 39.96922920035118665, 92.45433879953094447 ) ) ;
#12509=CARTESIAN_POINT ( 'NONE',  ( -4.622577041588897373, 46.56120873422322859, 95.06371379782397923 ) ) ;
#12522=ORIENTED_EDGE ( 'NONE', *, *, #17142, .T. ) ;
#12528=CARTESIAN_POINT ( 'NONE',  ( 0.7582201636353298468, 49.56899138526064519, 90.53246379953097289 ) ) ;
#12551=ORIENTED_EDGE ( 'NONE', *, *, #3647, .T. ) ;
#12552=CYLINDRICAL_SURFACE ( 'NONE', #10776, 6.999999999999999112 ) ;
#12583=CARTESIAN_POINT ( 'NONE',  ( -3.628867371436363509, 48.69222599884265179, 92.32933879782399345 ) ) ;
#12590=CARTESIAN_POINT ( 'NONE',  ( 5.052198367669452850, 48.31320248322254685, 94.67308879782399345 ) ) ;
#12613=CARTESIAN_POINT ( 'NONE',  ( -2.530020917761411692, 39.85184329928002001, 92.45433879953093026 ) ) ;
#12615=CARTESIAN_POINT ( 'NONE',  ( -1.419351766502867429, 49.49642391118513274, 92.40746379782397923 ) ) ;
#12630=ORIENTED_EDGE ( 'NONE', *, *, #20256, .F. ) ;
#12641=CARTESIAN_POINT ( 'NONE',  ( -4.176309363623029292, 42.45208065485131499, 92.17308879953097289 ) ) ;
#12647=DIRECTION ( 'NONE',  ( 0.000000000000000000, 0.000000000000000000, 1.000000000000000000 ) ) ;
#12717=CARTESIAN_POINT ( 'NONE',  ( 0.2541436421823696223, 38.02374091943176637, 95.45433879782399345 ) ) ;
#12757=ORIENTED_EDGE ( 'NONE', *, *, #17142, .F. ) ;
#12782=CARTESIAN_POINT ( 'NONE',  ( 4.476015245556088651, 47.52441691994293649, 92.45433879953091605 ) ) ;
#12790=CARTESIAN_POINT ( 'NONE',  ( 4.921111604934655048, 46.69516597009693726, 95.01862182907727572 ) ) ;
#12813=CARTESIAN_POINT ( 'NONE',  ( -1.876873622437039257, 39.01745058958429269, 92.87621379782399345 ) ) ;
#12838=CARTESIAN_POINT ( 'NONE',  ( 5.928963754087451576, 43.92611494815086814, 93.96996379953098710 ) ) ;
#12864=CARTESIAN_POINT ( 'NONE',  ( -5.356086414478568258, 43.71529702833873898, 92.51086634196040848 ) ) ;
#12924=CARTESIAN_POINT ( 'NONE',  ( 0.2860873169776699254, 38.75537135769874197, 94.59496379611701400 ) ) ;
#12935=CARTESIAN_POINT ( 'NONE',  ( 0.5221537403065085181, 49.16218137147969003, 93.04136871766880290 ) ) ;
#12946=VERTEX_POINT ( 'NONE', #12935 ) ;
#12949=CARTESIAN_POINT ( 'NONE',  ( 0.7901638384306286511, 50.30062182352762079, 92.17308879782397923 ) ) ;
#12954=UNCERTAINTY_MEASURE_WITH_UNIT (LENGTH_MEASURE( 1.000000000000000082E-05 ), #6145, 'distance_accuracy_value', 'NONE');
#12963=PLANE ( 'NONE',  #20759 ) ;
#12974=CARTESIAN_POINT ( 'NONE',  ( 5.666884522201895535, 41.76315400873614436, 93.03246379782397923 ) ) ;
#13029=CARTESIAN_POINT ( 'NONE',  ( -1.898293902487090401, 49.05989174320345114, 95.05433879953098142 ) ) ;
#13033=CARTESIAN_POINT ( 'NONE',  ( 4.178421596892071044, 40.17206517740157778, 92.25121379611699979 ) ) ;
#13034=CARTESIAN_POINT ( 'NONE',  ( -4.812088799398939187, 42.22067586467031930, 92.56371379782397923 ) ) ;
#13058=CARTESIAN_POINT ( 'NONE',  ( 2.232254456934870568, 39.46371826755015633, 94.98558879953097289 ) ) ;
#13074=EDGE_LOOP ( 'NONE', ( #3107, #20998, #6900, #2697 ) ) ;
#13083=CARTESIAN_POINT ( 'NONE',  ( 0.2541436421823703995, 38.02374091943176637, 94.04808879782399345 ) ) ;
#13115=CARTESIAN_POINT ( 'NONE',  ( 0.5221537403065006355, 44.16218137147969003, 92.45433879953097289 ) ) ;
#13131=CARTESIAN_POINT ( 'NONE',  ( 5.053692675489761754, 42.04909006277621586, 94.82933879611698558 ) ) ;
#13132=CARTESIAN_POINT ( 'NONE',  ( 5.856396280011940902, 46.10368687828906076, 91.93871379782397923 ) ) ;
#13137=ORIENTED_EDGE ( 'NONE', *, *, #20758, .T. ) ;
#13158=CARTESIAN_POINT ( 'NONE',  ( -4.009385194876762704, 46.27527268018315709, 94.51683879953097289 ) ) ;
#13173=DIRECTION ( 'NONE',  ( 5.626130192357176673E-16, 1.809130530872730902E-30, -1.000000000000000000 ) ) ;
#13185=CARTESIAN_POINT ( 'NONE',  ( 2.921181103050038086, 49.30691215337508737, 94.59496379782397923 ) ) ;
#13238=CARTESIAN_POINT ( 'NONE',  ( 0.2860873169776705915, 38.75537135769874197, 93.34496379611698558 ) ) ;
#13241=CARTESIAN_POINT ( 'NONE',  ( 0.5221537403065006355, 44.16218137147969003, 92.45433879953097289 ) ) ;
#13302=ADVANCED_FACE ( 'NONE', ( #11970 ), #13448, .T. ) ;
#13347=CARTESIAN_POINT ( 'NONE',  ( -4.884656273474451638, 44.39824779480852612, 94.28246379611698558 ) ) ;
#13348=CARTESIAN_POINT ( 'NONE',  ( -1.876873622437039257, 39.01745058958429269, 92.87621379782399345 ) ) ;
#13375=CARTESIAN_POINT ( 'NONE',  ( 4.178421596892070156, 40.17206517740157778, 93.81371379953098710 ) ) ;
#13397=CARTESIAN_POINT ( 'NONE',  ( -4.007890887056452023, 40.01116025973682611, 93.89183879782397923 ) ) ;
#13411=DIRECTION ( 'NONE',  ( 1.290716872006552287E-16, 1.000000000000000000, 0.000000000000000000 ) ) ;
#13439=CARTESIAN_POINT ( 'NONE',  ( -1.187946976321871961, 48.86064447540922373, 93.11058879953097289 ) ) ;
#13447=CARTESIAN_POINT ( 'NONE',  ( -4.007890887056452023, 40.01116025973682611, 94.04808879782397923 ) ) ;
#13448=CYLINDRICAL_SURFACE ( 'NONE', #3463, 4.999999999999997335 ) ;
#13546=CARTESIAN_POINT ( 'NONE',  ( 5.052198367669452850, 48.31320248322254685, 94.51683879782399345 ) ) ;
#13615=CARTESIAN_POINT ( 'NONE',  ( -2.313335635445065375, 50.56218137147968861, 96.05433879953096721 ) ) ;
#13629=EDGE_CURVE ( 'NONE', #14920, #6478, #9597, .T. ) ;
#13659=CARTESIAN_POINT ( 'NONE',  ( 2.921181103050038530, 49.30691215337508737, 93.50121379782399345 ) ) ;
#13699=CARTESIAN_POINT ( 'NONE',  ( -5.616286711741430793, 44.43019146960381960, 93.73558879782397923 ) ) ;
#13707=EDGE_CURVE ( 'NONE', #8776, #799, #10650, .T. ) ;
#13747=CARTESIAN_POINT ( 'NONE',  ( 0.2541436421823703440, 38.02374091943176637, 94.20433879782399345 ) ) ;
#13748=CARTESIAN_POINT ( 'NONE',  ( -1.590937568396970203, 39.63064243629642647, 94.82933879953097289 ) ) ;
#13762=CARTESIAN_POINT ( 'NONE',  ( 0.2541436421823703440, 38.02374091943176637, 94.20433879782400766 ) ) ;
#13775=CARTESIAN_POINT ( 'NONE',  ( -0.7270676699343749938, 38.96968808794299122, 95.05433879953099563 ) ) ;
#13785=CARTESIAN_POINT ( 'NONE',  ( 1.403788643848842055, 39.16218137147969003, 93.70233169107481785 ) ) ;
#13801=DIRECTION ( 'NONE',  ( -5.626130192357176673E-16, -1.831515347669941892E-30, 1.000000000000000000 ) ) ;
#13802=CARTESIAN_POINT ( 'NONE',  ( 2.635245049009970586, 48.69372030666295359, 90.45433879953097289 ) ) ;
#13864=CARTESIAN_POINT ( 'NONE',  ( 5.856396280011939126, 46.10368687828906076, 94.59496379782397923 ) ) ;
#13868=AXIS2_PLACEMENT_3D ( 'NONE', #6476, #11500, #6682 ) ;
#13873=ORIENTED_EDGE ( 'NONE', *, *, #19181, .F. ) ;
#13884=VERTEX_POINT ( 'NONE', #19028 ) ;
#13928=VECTOR ( 'NONE', #10487, 1000.000000000000000 ) ;
#13936=ORIENTED_EDGE ( 'NONE', *, *, #15889, .T. ) ;
#13970=CARTESIAN_POINT ( 'NONE',  ( -1.419351766502867873, 49.49642391118513274, 93.50121379782397923 ) ) ;
#13988=CARTESIAN_POINT ( 'NONE',  ( 3.394637663597737998, 39.16678726411793576, 95.40913173179340845 ) ) ;
#14000=CARTESIAN_POINT ( 'NONE',  ( 5.666884522201896424, 41.76315400873614436, 91.93871379782397923 ) ) ;
#14014=CARTESIAN_POINT ( 'NONE',  ( -4.609362567131230826, 46.70091906356311995, 92.45433879953098710 ) ) ;
#14018=CARTESIAN_POINT ( 'NONE',  ( -1.187946976321870629, 48.86064447540922373, 90.61058879953097289 ) ) ;
#14042=CARTESIAN_POINT ( 'NONE',  ( 0.5221537403064990812, 44.16218137147969003, 95.05433879953096721 ) ) ;
#14062=CARTESIAN_POINT ( 'NONE',  ( 5.856396280011939126, 46.10368687828906076, 94.59496379782397923 ) ) ;
#14077=CARTESIAN_POINT ( 'NONE',  ( 0.5221537403065040772, 39.16218137147969003, 94.91636871766883132 ) ) ;
#14079=CARTESIAN_POINT ( 'NONE',  ( -1.419351766502868761, 49.49642391118513274, 94.90746379782397923 ) ) ;
#14084=LINE ( 'NONE', #20568, #18348 ) ;
#14090=CARTESIAN_POINT ( 'NONE',  ( 4.178421596892070156, 40.17206517740157778, 93.50121379611698558 ) ) ;
#14098=CARTESIAN_POINT ( 'NONE',  ( -0.05336403213008323460, 39.08435147610357774, 92.45433879953100131 ) ) ;
#14100=CARTESIAN_POINT ( 'NONE',  ( 5.052198367669454626, 48.31320248322254685, 93.42308879782400766 ) ) ;
#14143=CARTESIAN_POINT ( 'NONE',  ( 0.5221537403064979710, 39.16218137147969003, 93.35386871425482980 ) ) ;
#14152=VERTEX_POINT ( 'NONE', #2299 ) ;
#14155=ORIENTED_EDGE ( 'NONE', *, *, #389, .F. ) ;
#14156=CARTESIAN_POINT ( 'NONE',  ( -1.419351766502868317, 49.49642391118513274, 93.65746379782397923 ) ) ;
#14171=CARTESIAN_POINT ( 'NONE',  ( -3.628867371436365730, 48.69222599884265179, 94.98558879782399345 ) ) ;
#14199=CARTESIAN_POINT ( 'NONE',  ( 6.660594192354429843, 43.89417127335556046, 93.26683879782399345 ) ) ;
#14223=ORIENTED_EDGE ( 'NONE', *, *, #5545, .T. ) ;
#14293=CARTESIAN_POINT ( 'NONE',  ( -5.060671531193845496, 45.43096853849363725, 95.05433879953096721 ) ) ;
#14306=CARTESIAN_POINT ( 'NONE',  ( 4.155794158978344477, 39.80096085272940343, 95.60097222790500382 ) ) ;
#14327=EDGE_CURVE ( 'NONE', #3932, #10333, #5817, .T. ) ;
#14332=( BOUNDED_CURVE ( )  B_SPLINE_CURVE ( 2, ( #12375, #12160, #10474, #18850, #12270, #16938, #4262, #10788, #18639, #20640, #18536, #1092, #2364, #4054, #9182, #17254, #14156, #3950, #17361, #7251, #5650, #10582, #1194, #13747, #15672, #8868, #7579, #15354, #14062, #20217, #17052, #20546, #18752, #9072, #976 ),
 .UNSPECIFIED., .F., .F. ) 
 B_SPLINE_CURVE_WITH_KNOTS ( ( 3, 2, 2, 2, 2, 2, 2, 2, 2, 2, 2, 2, 2, 2, 2, 2, 2, 3 ),
 ( 0.3161083822038468494, 0.3396651204095990084, 0.3736316324505708497, 0.4075981444915426355, 0.4415646565325144768, 0.4755311685734863181, 0.5094976806144581039, 0.5434641926554300007, 0.5774307046964017864, 0.6113972167373735722, 0.6453637287783454690, 0.6793302408193173658, 0.7132967528602891516, 0.7472632649012609374, 0.7812297769422327232, 0.8151962889832046200, 0.8491628010241764057, 0.8809549974670297656 ),
 .UNSPECIFIED. ) 
 CURVE ( )  GEOMETRIC_REPRESENTATION_ITEM ( )  RATIONAL_B_SPLINE_CURVE ( ( 0.9676416783630596985, 0.9472082996756301387, 1.000000000000000000, 0.9238795325112867385, 1.000000000000000000, 0.9238795325112867385, 1.000000000000000000, 0.9238795325112867385, 1.000000000000000000, 0.9238795325112867385, 1.000000000000000000, 0.9238795325112867385, 1.000000000000000000, 0.9238795325112867385, 1.000000000000000000, 0.9238795325112867385, 1.000000000000000000, 0.9238795325112867385, 1.000000000000000000, 0.9238795325112867385, 1.000000000000000000, 0.9238795325112867385, 1.000000000000000000, 0.9238795325112867385, 1.000000000000000000, 0.9238795325112867385, 1.000000000000000000, 0.9238795325112867385, 1.000000000000000000, 0.9238795325112867385, 1.000000000000000000, 0.9238795325112867385, 1.000000000000000000, 0.9287522706834349107, 0.9908783657858857286 ) ) 
 REPRESENTATION_ITEM ( '' )  );
#14334=CARTESIAN_POINT ( 'NONE',  ( -1.419351766502866541, 49.49642391118513274, 91.00121379782397923 ) ) ;
#14378=CARTESIAN_POINT ( 'NONE',  ( 3.725227782951431976, 48.32835457620019781, 92.45433879953095868 ) ) ;
#14408=VERTEX_POINT ( 'NONE', #19980 ) ;
#14409=CARTESIAN_POINT ( 'NONE',  ( 0.01393779443975506731, 49.47836700364563711, 95.05433879953096721 ) ) ;
#14412=CARTESIAN_POINT ( 'NONE',  ( 0.2541436421823710656, 38.02374091943176637, 92.95433879782399345 ) ) ;
#14420=CARTESIAN_POINT ( 'NONE',  ( 0.5221537403065085181, 49.16218137147969003, 93.04136871766880290 ) ) ;
#14434=CARTESIAN_POINT ( 'NONE',  ( 2.232254456934871900, 39.46371826755015633, 92.48558879953097289 ) ) ;
#14477=ORIENTED_EDGE ( 'NONE', *, *, #15206, .F. ) ;
#14479=CARTESIAN_POINT ( 'NONE',  ( 0.5221537403064990812, 44.16218137147969003, 95.05433879953096721 ) ) ;
#14502=CARTESIAN_POINT ( 'NONE',  ( 5.434012744193106315, 45.09686908721048582, 92.45433879953098710 ) ) ;
#14510=CARTESIAN_POINT ( 'NONE',  ( 0.6695212169850585093, 49.45709967392639328, 95.05433879953099563 ) ) ;
#14515=CARTESIAN_POINT ( 'NONE',  ( -1.187946976321872405, 48.86064447540922373, 94.04808879611699979 ) ) ;
#14518=CARTESIAN_POINT ( 'NONE',  ( -5.616286711741429905, 44.43019146960381960, 92.48558879782397923 ) ) ;
#14541=CARTESIAN_POINT ( 'NONE',  ( 0.2860873169776710356, 38.75537135769874197, 92.40746379953097289 ) ) ;
#14546=VECTOR ( 'NONE', #9505, 1000.000000000000000 ) ;
#14547=( NAMED_UNIT ( * ) PLANE_ANGLE_UNIT ( ) SI_UNIT ( $, .RADIAN. ) );
#14551=EDGE_CURVE ( 'NONE', #14408, #9268, #18439, .T. ) ;
#14589=CARTESIAN_POINT ( 'NONE',  ( -2.627048034785010699, 48.88511640015991588, 92.45433879952862810 ) ) ;
#14602=ORIENTED_EDGE ( 'NONE', *, *, #3647, .F. ) ;
#14622=CARTESIAN_POINT ( 'NONE',  ( 4.178421596892070156, 40.17206517740157778, 94.75121379611699979 ) ) ;
#14624=CARTESIAN_POINT ( 'NONE',  ( -3.628867371436363953, 48.69222599884265179, 93.57933879782399345 ) ) ;
#14630=CARTESIAN_POINT ( 'NONE',  ( 2.635245049009969254, 48.69372030666295359, 92.95433879953098710 ) ) ;
#14684=AXIS2_PLACEMENT_3D ( 'NONE', #7916, #139, #9834 ) ;
#14692=CARTESIAN_POINT ( 'NONE',  ( -1.842009727706052091, 49.28276247982005742, 92.45433879953100131 ) ) ;
#14698=EDGE_CURVE ( 'NONE', #9268, #14408, #1119, .T. ) ;
#14701=CARTESIAN_POINT ( 'NONE',  ( 1.403788643848841833, 39.16218137147969003, 94.63983168766084475 ) ) ;
#14720=EDGE_LOOP ( 'NONE', ( #2992, #12269, #19253, #15060 ) ) ;
#14727=CARTESIAN_POINT ( 'NONE',  ( 0.2860873169776692038, 38.75537135769874197, 95.84496379611699979 ) ) ;
#14728=CARTESIAN_POINT ( 'NONE',  ( 4.673174852049362116, 39.63213674411673537, 92.95433879782399345 ) ) ;
#14791=CARTESIAN_POINT ( 'NONE',  ( -3.134114116279072881, 48.15229756555780227, 94.12621379611699979 ) ) ;
#14806=VERTEX_POINT ( 'NONE', #4698 ) ;
#14814=EDGE_CURVE ( 'NONE', #3900, #10995, #6976, .T. ) ;
#14824=DIRECTION ( 'NONE',  ( -5.626130192357176673E-16, -1.831515347669941892E-30, 1.000000000000000000 ) ) ;
#14826=EDGE_CURVE ( 'NONE', #18462, #2266, #16376, .T. ) ;
#14829=CARTESIAN_POINT ( 'NONE',  ( 5.666884522201896424, 41.76315400873614436, 91.78246379782397923 ) ) ;
#14851=VECTOR ( 'NONE', #14824, 1000.000000000000000 ) ;
#14875=CARTESIAN_POINT ( 'NONE',  ( -1.876873622437039257, 39.01745058958429269, 92.71996379782397923 ) ) ;
#14908=AXIS2_PLACEMENT_3D ( 'NONE', #14479, #17257, #10894 ) ;
#14920=VERTEX_POINT ( 'NONE', #14502 ) ;
#14929=CARTESIAN_POINT ( 'NONE',  ( 5.053692675489762642, 42.04909006277621586, 92.32933879611698558 ) ) ;
#14931=CARTESIAN_POINT ( 'NONE',  ( -3.628867371436365730, 48.69222599884265179, 94.82933879782397923 ) ) ;
#14947=AXIS2_PLACEMENT_3D ( 'NONE', #13115, #6824, #18114 ) ;
#14989=CARTESIAN_POINT ( 'NONE',  ( -4.007890887056451135, 40.01116025973682611, 92.64183879782400766 ) ) ;
#15047=CARTESIAN_POINT ( 'NONE',  ( -4.622577041588897373, 46.56120873422322859, 94.90746379782396502 ) ) ;
#15050=ADVANCED_FACE ( 'NONE', ( #18910 ), #9997, .F. ) ;
#15060=ORIENTED_EDGE ( 'NONE', *, *, #19181, .T. ) ;
#15061=LINE ( 'NONE', #3565, #5433 ) ;
#15071=DIRECTION ( 'NONE',  ( 1.000000000000000000, 4.924280921909908032E-16, 5.626130192357177659E-16 ) ) ;
#15098=CARTESIAN_POINT ( 'NONE',  ( 0.2541436421823711211, 38.02374091943176637, 92.79808879782399345 ) ) ;
#15131=UNCERTAINTY_MEASURE_WITH_UNIT (LENGTH_MEASURE( 1.000000000000000082E-05 ), #93, 'distance_accuracy_value', 'NONE');
#15151=CARTESIAN_POINT ( 'NONE',  ( 3.722852957781953798, 40.32059543431686421, 95.05433879953096721 ) ) ;
#15152=CARTESIAN_POINT ( 'NONE',  ( -4.007890887056448470, 40.01116025973682611, 91.54808879782400766 ) ) ;
#15175=CARTESIAN_POINT ( 'NONE',  ( 1.630627053521186864, 49.16218137147969003, 94.24615272619178086 ) ) ;
#15194=ADVANCED_FACE ( 'NONE', ( #11642 ), #233, .T. ) ;
#15206=EDGE_CURVE ( 'NONE', #14920, #13884, #4923, .T. ) ;
#15229=CARTESIAN_POINT ( 'NONE',  ( -0.3594811632358396736, 49.16218137147969003, 92.76483168766085896 ) ) ;
#15257=LINE ( 'NONE', #15468, #13928 ) ;
#15259=CARTESIAN_POINT ( 'NONE',  ( 4.673174852049362116, 39.63213674411673537, 93.11058879782397923 ) ) ;
#15262=ORIENTED_EDGE ( 'NONE', *, *, #14814, .F. ) ;
#15354=CARTESIAN_POINT ( 'NONE',  ( 6.660594192354428955, 43.89417127335556046, 94.51683879782399345 ) ) ;
#15355=CARTESIAN_POINT ( 'NONE',  ( 0.5221537403065076299, 49.16218137147969003, 94.29136871766880290 ) ) ;
#15366=EDGE_CURVE ( 'NONE', #11953, #18462, #14332, .T. ) ;
#15371=CARTESIAN_POINT ( 'NONE',  ( 5.052198367669454626, 48.31320248322254685, 93.42308879782400766 ) ) ;
#15412=CARTESIAN_POINT ( 'NONE',  ( 5.928963754087452465, 43.92611494815086814, 91.46996379953098710 ) ) ;
#15429=EDGE_CURVE ( 'NONE', #17689, #20491, #20829, .T. ) ;
#15468=CARTESIAN_POINT ( 'NONE',  ( 0.5221537403065017457, 49.16218137147969003, 92.45433879953097289 ) ) ;
#15472=CARTESIAN_POINT ( 'NONE',  ( 0.2541436421823696223, 38.02374091943176637, 95.45433879782399345 ) ) ;
#15486=CARTESIAN_POINT ( 'NONE',  ( -4.622577041588897373, 46.56120873422322859, 94.90746379782396502 ) ) ;
#15496=CARTESIAN_POINT ( 'NONE',  ( -4.342627717588348091, 41.70135421888197413, 92.45433879953091605 ) ) ;
#15516=CARTESIAN_POINT ( 'NONE',  ( -3.467962453771610054, 40.50591351489412517, 91.00121379953098710 ) ) ;
#15623=VECTOR ( 'NONE', #13801, 1000.000000000000000 ) ;
#15672=CARTESIAN_POINT ( 'NONE',  ( 2.463659247115866258, 38.82793883177424732, 94.28246379782397923 ) ) ;
#15675=CARTESIAN_POINT ( 'NONE',  ( 0.5221537403065006355, 44.16218137147969003, 92.45433879953097289 ) ) ;
#15708=CARTESIAN_POINT ( 'NONE',  ( -0.7071044773352802570, 39.15572691966126229, 92.45433879953097289 ) ) ;
#15711=CARTESIAN_POINT ( 'NONE',  ( -3.628867371436365730, 48.69222599884265179, 94.98558879782399345 ) ) ;
#15733=CARTESIAN_POINT ( 'NONE',  ( 2.635245049009970142, 48.69372030666295359, 91.70433879953097289 ) ) ;
#15742=EDGE_CURVE ( 'NONE', #4231, #11953, #20390, .T. ) ;
#15805=CARTESIAN_POINT ( 'NONE',  ( 5.053692675489762642, 42.04909006277621586, 93.57933879611698558 ) ) ;
#15816=CARTESIAN_POINT ( 'NONE',  ( -1.419351766502866541, 49.49642391118513274, 91.15746379782397923 ) ) ;
#15889=EDGE_CURVE ( 'NONE', #12110, #14806, #16217, .T. ) ;
#15914=CARTESIAN_POINT ( 'NONE',  ( -4.812088799398940075, 42.22067586467031930, 95.21996379782397923 ) ) ;
#15924=CARTESIAN_POINT ( 'NONE',  ( 2.232254456934871900, 39.46371826755015633, 92.48558879953097289 ) ) ;
#15927=DIRECTION ( 'NONE',  ( -5.626130192357176673E-16, -1.831515347669941892E-30, 1.000000000000000000 ) ) ;
#15985=CARTESIAN_POINT ( 'NONE',  ( 2.037483459743116843, 49.33852326317117587, 92.45433879953093026 ) ) ;
#16015=CARTESIAN_POINT ( 'NONE',  ( 3.294548648621552278, 48.45522119969754016, 95.05433879953096721 ) ) ;
#16020=CARTESIAN_POINT ( 'NONE',  ( 5.856396280011940014, 46.10368687828906076, 93.34496379782399345 ) ) ;
#16041=CIRCLE ( 'NONE', #14684, 6.999999999999999112 ) ;
#16045=CARTESIAN_POINT ( 'NONE',  ( -4.884656273474451638, 44.39824779480852612, 94.59496379953098710 ) ) ;
#16064=AXIS2_PLACEMENT_3D ( 'NONE', #18511, #5200, #13411 ) ;
#16088=CARTESIAN_POINT ( 'NONE',  ( 3.213865265001516480, 48.74132121123690808, 92.45433879953098710 ) ) ;
#16113=CYLINDRICAL_SURFACE ( 'NONE', #4800, 4.200000000000001954 ) ;
#16118=ORIENTED_EDGE ( 'NONE', *, *, #10699, .T. ) ;
#16123=CARTESIAN_POINT ( 'NONE',  ( 4.673174852049363004, 39.63213674411673537, 91.86058879782397923 ) ) ;
#16124=CARTESIAN_POINT ( 'NONE',  ( -4.007890887056451135, 40.01116025973682611, 92.64183879782400766 ) ) ;
#16133=PRODUCT_DEFINITION ( 'UNKNOWN', '', #706, #9980 ) ;
#16148=CARTESIAN_POINT ( 'NONE',  ( 2.921181103050039418, 49.30691215337508737, 92.09496379782399345 ) ) ;
#16149=ORIENTED_EDGE ( 'NONE', *, *, #389, .T. ) ;
#16153=CARTESIAN_POINT ( 'NONE',  ( 0.000000000000000000, 0.000000000000000000, 0.000000000000000000 ) ) ;
#16168=( NAMED_UNIT ( * ) PLANE_ANGLE_UNIT ( ) SI_UNIT ( $, .RADIAN. ) );
#16195=( BOUNDED_CURVE ( )  B_SPLINE_CURVE ( 2, ( #11039, #19203, #15924, #6122, #2933, #1450, #3249, #2834, #14630, #6538, #14420 ),
 .UNSPECIFIED., .F., .T. ) 
 B_SPLINE_CURVE_WITH_KNOTS ( ( 3, 2, 2, 2, 2, 3 ),
 ( 0.3997652871908818351, 0.4062500000000000000, 0.4375000000000000000, 0.4687500000000000000, 0.5000000000000000000, 0.5173390146554853741 ),
 .UNSPECIFIED. ) 
 CURVE ( )  GEOMETRIC_REPRESENTATION_ITEM ( )  RATIONAL_B_SPLINE_CURVE ( ( 0.9749639670273970715, 0.9842041801420761127, 1.000000000000000000, 0.9238795325112867385, 1.000000000000000000, 0.9238795325112867385, 1.000000000000000000, 0.9238795325112867385, 1.000000000000000000, 0.9577646751561856853, 0.9623977609649205789 ) ) 
 REPRESENTATION_ITEM ( '' )  );
#16213=EDGE_CURVE ( 'NONE', #4231, #2266, #11614, .T. ) ;
#16217=LINE ( 'NONE', #9637, #2147 ) ;
#16222=CARTESIAN_POINT ( 'NONE',  ( -4.884656273474452526, 44.39824779480852612, 95.53246379611698558 ) ) ;
#16224=CARTESIAN_POINT ( 'NONE',  ( 0.7901638384306278740, 50.30062182352762079, 93.42308879782399345 ) ) ;
#16325=VECTOR ( 'NONE', #11529, 1000.000000000000000 ) ;
#16328=CARTESIAN_POINT ( 'NONE',  ( 2.548566262980702213, 48.91524988949119290, 95.05433879953096721 ) ) ;
#16331=CARTESIAN_POINT ( 'NONE',  ( -1.590937568396971091, 39.63064243629642647, 95.76683879611698558 ) ) ;
#16333=CARTESIAN_POINT ( 'NONE',  ( 0.2541436421823711211, 38.02374091943176637, 92.79808879782397923 ) ) ;
#16351=ORIENTED_EDGE ( 'NONE', *, *, #19611, .F. ) ;
#16354=CARTESIAN_POINT ( 'NONE',  ( -4.009385194876761815, 46.27527268018315709, 93.26683879953097289 ) ) ;
#16376=B_SPLINE_CURVE_WITH_KNOTS ( 'NONE', 3,
 ( #1323, #7808, #14293, #18882, #20769, #1531 ),
 .UNSPECIFIED., .F., .F.,
 ( 4, 2, 4 ),
 ( 0.000000000000000000, 0.002233029297497547087, 0.004466058594995094173 ),
 .UNSPECIFIED. ) ;
#16410=ADVANCED_FACE ( 'NONE', ( #4095 ), #19351, .F. ) ;
#16428=CARTESIAN_POINT ( 'NONE',  ( 0.5221537403065015237, 49.16218137147969003, 92.72886871425484401 ) ) ;
#16431=DIRECTION ( 'NONE',  ( 1.239088197126290817E-16, 1.000000000000000000, 0.000000000000000000 ) ) ;
#16434=EDGE_LOOP ( 'NONE', ( #8751, #11837, #19905, #20987 ) ) ;
#16437=ORIENTED_EDGE ( 'NONE', *, *, #14698, .T. ) ;
#16441=CARTESIAN_POINT ( 'NONE',  ( -4.176309363623030180, 42.45208065485131499, 93.11058879611698558 ) ) ;
#16484=CARTESIAN_POINT ( 'NONE',  ( 0.7901638384306279850, 50.30062182352762079, 93.42308879782399345 ) ) ;
#16490=ORIENTED_EDGE ( 'NONE', *, *, #3242, .T. ) ;
#16501=CARTESIAN_POINT ( 'NONE',  ( -4.176309363623031068, 42.45208065485131499, 94.36058879611698558 ) ) ;
#16587=CARTESIAN_POINT ( 'NONE',  ( -1.419351766502868761, 49.49642391118513274, 94.75121379782397923 ) ) ;
#16609=VERTEX_POINT ( 'NONE', #14077 ) ;
#16625=CARTESIAN_POINT ( 'NONE',  ( 0.5221537403065017457, 49.16218137147969003, 92.45433879953097289 ) ) ;
#16644=CARTESIAN_POINT ( 'NONE',  ( 5.220616844236031007, 45.87228208810806507, 92.48558879611698558 ) ) ;
#16645=CARTESIAN_POINT ( 'NONE',  ( 2.921181103050038086, 49.30691215337508737, 94.59496379782397923 ) ) ;
#16700=CARTESIAN_POINT ( 'NONE',  ( 0.5221537403065006355, 44.16218137147969003, 92.45433879953097289 ) ) ;
#16744=CARTESIAN_POINT ( 'NONE',  ( -3.541825984438901731, 47.99675089776317805, 95.05433879953095300 ) ) ;
#16751=CARTESIAN_POINT ( 'NONE',  ( 6.660594192354429843, 43.89417127335556046, 94.36058879782399345 ) ) ;
#16766=CARTESIAN_POINT ( 'NONE',  ( 1.233827257842946334, 39.01589007119768837, 95.05433879953096721 ) ) ;
#16778=CARTESIAN_POINT ( 'NONE',  ( 5.220616844236030119, 45.87228208810806507, 94.04808879953097289 ) ) ;
#16826=LINE ( 'NONE', #8743, #9197 ) ;
#16846=DIRECTION ( 'NONE',  ( 5.626130192357176673E-16, 1.809130530872730902E-30, -1.000000000000000000 ) ) ;
#16853=CARTESIAN_POINT ( 'NONE',  ( 6.660594192354429843, 43.89417127335556046, 92.01683879782399345 ) ) ;
#16938=CARTESIAN_POINT ( 'NONE',  ( -4.007890887056451135, 40.01116025973682611, 92.79808879782399345 ) ) ;
#16950=CARTESIAN_POINT ( 'NONE',  ( -2.313335635445063154, 37.76218137147968434, 92.03489701350649455 ) ) ;
#16954=CARTESIAN_POINT ( 'NONE',  ( -1.876873622437040590, 39.01745058958429269, 95.21996379782397923 ) ) ;
#16967=CARTESIAN_POINT ( 'NONE',  ( -4.546431600613201951, 41.68282864742221250, 95.05433879953095300 ) ) ;
#16968=CARTESIAN_POINT ( 'NONE',  ( 0.5221537403065006355, 44.16218137147969003, 92.45433879953097289 ) ) ;
#16979=ADVANCED_FACE ( 'NONE', ( #1544 ), #18117, .F. ) ;
#17001=CARTESIAN_POINT ( 'NONE',  ( 3.357643116058062205, 50.56218137147968861, 92.03489701350649455 ) ) ;
#17003=AXIS2_PLACEMENT_3D ( 'NONE', #9277, #10566, #19053 ) ;
#17052=CARTESIAN_POINT ( 'NONE',  ( 2.921181103050038086, 49.30691215337508737, 94.75121379782399345 ) ) ;
#17068=CARTESIAN_POINT ( 'NONE',  ( 4.673174852049361228, 39.63213674411673537, 94.36058879782399345 ) ) ;
#17078=ORIENTED_EDGE ( 'NONE', *, *, #9388, .F. ) ;
#17093=B_SPLINE_CURVE_WITH_KNOTS ( 'NONE', 3,
 ( #10502, #20148, #16967, #20248, #6955, #3771, #12083, #8899, #5360, #4196, #12301, #13775, #10722, #3875, #20041, #17182, #16766, #10290, #578, #2605, #18459, #5677, #4086, #8684 ),
 .UNSPECIFIED., .F., .F.,
 ( 4, 2, 2, 2, 2, 2, 2, 2, 2, 2, 2, 4 ),
 ( 0.000000000000000000, 0.001310659670290844356, 0.001965989505436258403, 0.002621319340581672232, 0.003931979010872510734, 0.005242638681163349669, 0.006553298351454187737, 0.007208628186599608072, 0.007863958021745026672, 0.008519287856890446139, 0.009174617692035867342, 0.01048527736232670628 ),
 .UNSPECIFIED. ) ;
#17142=EDGE_CURVE ( 'NONE', #17381, #8776, #20277, .T. ) ;
#17161=FACE_BOUND ( 'NONE', #13074, .T. ) ;
#17180=CARTESIAN_POINT ( 'NONE',  ( -1.419351766502868761, 49.49642391118513274, 94.75121379782397923 ) ) ;
#17182=CARTESIAN_POINT ( 'NONE',  ( 1.018894512563303545, 38.97592790927090789, 95.05433879953099563 ) ) ;
#17205=CARTESIAN_POINT ( 'NONE',  ( -3.781340262490589410, 47.93810351720699003, 92.45433879953095868 ) ) ;
#17237=CARTESIAN_POINT ( 'NONE',  ( -3.134114116279072437, 48.15229756555780227, 92.87621379611698558 ) ) ;
#17251=B_SPLINE_CURVE_WITH_KNOTS ( 'NONE', 3,
 ( #14589, #116, #14692, #4578, #9498, #4996, #9396, #11515, #3208, #6182, #15985, #17569, #16088, #14378, #20853, #6281, #12782, #1728, #6490, #9811, #20949, #19369, #4783 ),
 .UNSPECIFIED., .F., .F.,
 ( 4, 2, 2, 2, 2, 2, 2, 2, 1, 2, 2, 4 ),
 ( 0.000000000000000000, 0.001314694893350534972, 0.001972042340025802459, 0.002629389786701069945, 0.003944084680051604917, 0.005258779573402139890, 0.006573474466752676597, 0.007230821913427943649, 0.007888169360103209835, 0.008545516806778478622, 0.009202864253453745674, 0.01051755914680430060 ),
 .UNSPECIFIED. ) ;
#17254=CARTESIAN_POINT ( 'NONE',  ( 0.7901638384306279850, 50.30062182352762079, 93.57933879782396502 ) ) ;
#17257=DIRECTION ( 'NONE',  ( 5.626130192357176673E-16, 1.831515347669941892E-30, -1.000000000000000000 ) ) ;
#17292=CARTESIAN_POINT ( 'NONE',  ( 5.856396280011939126, 46.10368687828906076, 94.59496379782397923 ) ) ;
#17318=CARTESIAN_POINT ( 'NONE',  ( -1.590937568396968649, 39.63064243629642647, 91.07933879953097289 ) ) ;
#17355=ORIENTED_EDGE ( 'NONE', *, *, #1938, .T. ) ;
#17361=CARTESIAN_POINT ( 'NONE',  ( -4.622577041588897373, 46.56120873422322859, 93.81371379782397923 ) ) ;
#17374=CARTESIAN_POINT ( 'NONE',  ( 4.359773538758245692, 47.36728266200564263, 95.05433879953096721 ) ) ;
#17375=CARTESIAN_POINT ( 'NONE',  ( 5.666884522201894647, 41.76315400873614436, 94.43871379782397923 ) ) ;
#17381=VERTEX_POINT ( 'NONE', #11661 ) ;
#17397=CARTESIAN_POINT ( 'NONE',  ( -3.233102370063162034, 40.36700684672312889, 92.45433879953093026 ) ) ;
#17400=CARTESIAN_POINT ( 'NONE',  ( -3.628867371436362621, 48.69222599884265179, 91.23558879782397923 ) ) ;
#17408=VECTOR ( 'NONE', #17760, 1000.000000000000000 ) ;
#17422=CARTESIAN_POINT ( 'NONE',  ( -3.134114116279071549, 48.15229756555780227, 91.93871379953098710 ) ) ;
#17475=CARTESIAN_POINT ( 'NONE',  ( 0.2541436421823711211, 38.02374091943176637, 92.79808879782397923 ) ) ;
#17481=CARTESIAN_POINT ( 'NONE',  ( -4.812088799398940075, 42.22067586467031930, 95.21996379782397923 ) ) ;
#17501=CARTESIAN_POINT ( 'NONE',  ( 4.673174852049361228, 39.63213674411673537, 94.36058879782399345 ) ) ;
#17524=CARTESIAN_POINT ( 'NONE',  ( -1.590937568396968871, 39.63064243629642647, 92.32933879953097289 ) ) ;
#17569=CARTESIAN_POINT ( 'NONE',  ( 2.841819011512540794, 48.97028086682659875, 92.45433879953095868 ) ) ;
#17588=CARTESIAN_POINT ( 'NONE',  ( 5.928963754087450688, 43.92611494815086814, 93.65746379611699979 ) ) ;
#17600=CARTESIAN_POINT ( 'NONE',  ( -1.419351766502868761, 49.49642391118513274, 94.90746379782397923 ) ) ;
#17621=CARTESIAN_POINT ( 'NONE',  ( -4.007890887056448470, 40.01116025973682611, 91.39183879782399345 ) ) ;
#17679=( GEOMETRIC_REPRESENTATION_CONTEXT ( 3 ) GLOBAL_UNCERTAINTY_ASSIGNED_CONTEXT ( ( #12954 ) ) GLOBAL_UNIT_ASSIGNED_CONTEXT ( ( #6145, #14547, #7957 ) ) REPRESENTATION_CONTEXT ( 'NONE', 'WORKASPACE' ) );
#17689=VERTEX_POINT ( 'NONE', #20633 ) ;
#17702=DIRECTION ( 'NONE',  ( -1.290716872006552287E-16, -1.000000000000000000, 0.000000000000000000 ) ) ;
#17710=CARTESIAN_POINT ( 'NONE',  ( 6.660594192354429843, 43.89417127335556046, 92.01683879782399345 ) ) ;
#17711=CARTESIAN_POINT ( 'NONE',  ( -1.876873622437039257, 39.01745058958429269, 92.71996379782397923 ) ) ;
#17734=CARTESIAN_POINT ( 'NONE',  ( 5.856396280011940902, 46.10368687828906076, 91.93871379782397923 ) ) ;
#17754=ORIENTED_EDGE ( 'NONE', *, *, #4634, .F. ) ;
#17758=PRESENTATION_STYLE_ASSIGNMENT (( #17858 ) ) ;
#17760=DIRECTION ( 'NONE',  ( -1.000000000000000000, -4.924280921909907046E-16, -5.626130192357177659E-16 ) ) ;
#17813=CARTESIAN_POINT ( 'NONE',  ( -3.134114116279073770, 48.15229756555780227, 95.37621379611701400 ) ) ;
#17814=CARTESIAN_POINT ( 'NONE',  ( 5.052198367669454626, 48.31320248322254685, 93.26683879782399345 ) ) ;
#17836=CARTESIAN_POINT ( 'NONE',  ( -1.590937568396970203, 39.63064243629642647, 94.82933879953097289 ) ) ;
#17855=ORIENTED_EDGE ( 'NONE', *, *, #3242, .F. ) ;
#17858=SURFACE_STYLE_USAGE ( .BOTH. , #9691 ) ;
#17868=VERTEX_POINT ( 'NONE', #11298 ) ;
#17878=CARTESIAN_POINT ( 'NONE',  ( -4.009385194876762704, 46.27527268018315709, 94.20433879611698558 ) ) ;
#17914=CARTESIAN_POINT ( 'NONE',  ( -1.590937568396968871, 39.63064243629642647, 92.01683879611699979 ) ) ;
#17916=CARTESIAN_POINT ( 'NONE',  ( -3.628867371436362621, 48.69222599884265179, 91.07933879782399345 ) ) ;
#17933=CIRCLE ( 'NONE', #1624, 4.200000000000001954 ) ;
#17940=CARTESIAN_POINT ( 'NONE',  ( 2.463659247115867590, 38.82793883177424732, 91.62621379782397923 ) ) ;
#18005=AXIS2_PLACEMENT_3D ( 'NONE', #20975, #20577, #17702 ) ;
#18023=CARTESIAN_POINT ( 'NONE',  ( 0.7582201636353285146, 49.56899138526064519, 92.71996379611701400 ) ) ;
#18048=CARTESIAN_POINT ( 'NONE',  ( -1.590937568396969759, 39.63064243629642647, 93.57933879953097289 ) ) ;
#18065=CARTESIAN_POINT ( 'NONE',  ( 0.5221537403064985261, 44.16218137147969003, 96.05433879953096721 ) ) ;
#18078=CARTESIAN_POINT ( 'NONE',  ( 6.660594192354430731, 43.89417127335556046, 93.11058879782397923 ) ) ;
#18114=DIRECTION ( 'NONE',  ( -1.301042606982606060E-16, -1.000000000000000000, 0.000000000000000000 ) ) ;
#18117=( BOUNDED_SURFACE ( )  B_SPLINE_SURFACE ( 1, 2, ( 
 ( #6528, #9644, #7926, #17916, #6631, #1762, #19297, #8347, #10058, #11240, #11656, #19404, #14829, #3239, #13132, #8029, #9844, #4711, #3554, #19718, #11443, #14518, #13034, #16124, #17711, #16333, #19607, #14728, #20982, #246, #4823, #17814, #18133, #16224, #6735, #14624, #5030, #149, #11549, #3446, #9959, #5136, #10384, #10600, #564, #16751, #8449, #13546, #16645, #20021, #3861, #14931, #15047, #20234, #11757, #5345, #16954, #10490, #18335, #787, #8883, #18231, #5456 ),
 ( #3651, #7047, #355, #2172, #1958, #6842, #11969, #15152, #3752, #10275, #18446, #5666, #678, #16853, #11857, #7157, #18551, #2065, #5241, #8771, #5568, #2270, #2383, #8671, #13348, #19819, #6942, #15259, #10163, #19919, #12071, #15371, #13659, #8562, #7268, #12176, #461, #20133, #18654, #13447, #3964, #13762, #4073, #17068, #17375, #7373, #13864, #12590, #10802, #7596, #14079, #14171, #11009, #12288, #17481, #12389, #1107, #15472, #20560, #20344, #1311, #18867, #20459 ) ),
 .UNSPECIFIED., .F., .F., .F. ) 
 B_SPLINE_SURFACE_WITH_KNOTS ( ( 2, 2 ),
 ( 3, 2, 2, 2, 2, 2, 2, 2, 2, 2, 2, 2, 2, 2, 2, 2, 2, 2, 2, 2, 2, 2, 2, 2, 2, 2, 2, 2, 2, 2, 2, 3 ),
 ( 0.000000000000000000, 1.000000000000000000 ),
 ( 0.000000000000000000, 0.03125000000000000000, 0.06250000000000000000, 0.09375000000000000000, 0.1250000000000000000, 0.1562500000000000000, 0.1875000000000000000, 0.2187500000000000000, 0.2500000000000000000, 0.2812500000000000000, 0.3125000000000000000, 0.3437500000000000000, 0.3750000000000000000, 0.4062500000000000000, 0.4375000000000000000, 0.4687500000000000000, 0.5000000000000000000, 0.5312500000000000000, 0.5625000000000000000, 0.5937500000000000000, 0.6250000000000000000, 0.6562500000000000000, 0.6875000000000000000, 0.7187500000000000000, 0.7500000000000000000, 0.7812500000000000000, 0.8125000000000000000, 0.8437500000000000000, 0.8750000000000000000, 0.9062500000000000000, 0.9200238152893590593, 0.9292240534422526732 ),
 .UNSPECIFIED. ) 
 GEOMETRIC_REPRESENTATION_ITEM ( )  RATIONAL_B_SPLINE_SURFACE ( (
 ( 1.000000000000000000, 0.9238795325112867385, 1.000000000000000000, 0.9238795325112867385, 1.000000000000000000, 0.9238795325112867385, 1.000000000000000000, 0.9238795325112867385, 1.000000000000000000, 0.9238795325112867385, 1.000000000000000000, 0.9238795325112867385, 1.000000000000000000, 0.9238795325112867385, 1.000000000000000000, 0.9238795325112867385, 1.000000000000000000, 0.9238795325112867385, 1.000000000000000000, 0.9238795325112867385, 1.000000000000000000, 0.9238795325112867385, 1.000000000000000000, 0.9238795325112867385, 1.000000000000000000, 0.9238795325112867385, 1.000000000000000000, 0.9238795325112867385, 1.000000000000000000, 0.9238795325112867385, 1.000000000000000000, 0.9238795325112867385, 1.000000000000000000, 0.9238795325112867385, 1.000000000000000000, 0.9238795325112867385, 1.000000000000000000, 0.9238795325112867385, 1.000000000000000000, 0.9238795325112867385, 1.000000000000000000, 0.9238795325112867385, 1.000000000000000000, 0.9238795325112867385, 1.000000000000000000, 0.9238795325112867385, 1.000000000000000000, 0.9238795325112867385, 1.000000000000000000, 0.9238795325112867385, 1.000000000000000000, 0.9238795325112867385, 1.000000000000000000, 0.9238795325112867385, 1.000000000000000000, 0.9238795325112867385, 1.000000000000000000, 0.9238795325112867385, 1.000000000000000000, 0.9664489837142656858, 0.9624739994982902669, 0.9624739994982902669, 0.9624739994982902669),
 ( 1.000000000000000000, 0.9238795325112867385, 1.000000000000000000, 0.9238795325112867385, 1.000000000000000000, 0.9238795325112867385, 1.000000000000000000, 0.9238795325112867385, 1.000000000000000000, 0.9238795325112867385, 1.000000000000000000, 0.9238795325112867385, 1.000000000000000000, 0.9238795325112867385, 1.000000000000000000, 0.9238795325112867385, 1.000000000000000000, 0.9238795325112867385, 1.000000000000000000, 0.9238795325112867385, 1.000000000000000000, 0.9238795325112867385, 1.000000000000000000, 0.9238795325112867385, 1.000000000000000000, 0.9238795325112867385, 1.000000000000000000, 0.9238795325112867385, 1.000000000000000000, 0.9238795325112867385, 1.000000000000000000, 0.9238795325112867385, 1.000000000000000000, 0.9238795325112867385, 1.000000000000000000, 0.9238795325112867385, 1.000000000000000000, 0.9238795325112867385, 1.000000000000000000, 0.9238795325112867385, 1.000000000000000000, 0.9238795325112867385, 1.000000000000000000, 0.9238795325112867385, 1.000000000000000000, 0.9238795325112867385, 1.000000000000000000, 0.9238795325112867385, 1.000000000000000000, 0.9238795325112867385, 1.000000000000000000, 0.9238795325112867385, 1.000000000000000000, 0.9238795325112867385, 1.000000000000000000, 0.9238795325112867385, 1.000000000000000000, 0.9238795325112867385, 1.000000000000000000, 0.9664489837142656858, 0.9624739994982902669, 0.9624739994982902669, 0.9624739994982902669) ) ) 
 REPRESENTATION_ITEM ( '' )  SURFACE ( )  );
#18133=CARTESIAN_POINT ( 'NONE',  ( 2.921181103050038974, 49.30691215337508737, 93.34496379782397923 ) ) ;
#18180=CARTESIAN_POINT ( 'NONE',  ( 6.660594192354428955, 43.89417127335556046, 94.36058879782399345 ) ) ;
#18194=EDGE_LOOP ( 'NONE', ( #14155, #13137, #7850, #1897 ) ) ;
#18220=DIRECTION ( 'NONE',  ( 5.626130192357176673E-16, 1.831515347669941892E-30, -1.000000000000000000 ) ) ;
#18230=CARTESIAN_POINT ( 'NONE',  ( -4.884656273474450749, 44.39824779480852612, 93.03246379611699979 ) ) ;
#18231=CARTESIAN_POINT ( 'NONE',  ( 4.666303754810079418, 40.22630141247467606, 95.46859283304921462 ) ) ;
#18270=ORIENTED_EDGE ( 'NONE', *, *, #18796, .F. ) ;
#18335=CARTESIAN_POINT ( 'NONE',  ( 2.463659247115865814, 38.82793883177424732, 95.37621379782397923 ) ) ;
#18336=DIRECTION ( 'NONE',  ( -5.626130192357176673E-16, -1.831515347669941892E-30, 1.000000000000000000 ) ) ;
#18339=ORIENTED_EDGE ( 'NONE', *, *, #18926, .T. ) ;
#18348=VECTOR ( 'NONE', #2278, 1000.000000000000000 ) ;
#18366=AXIS2_PLACEMENT_3D ( 'NONE', #16153, #12647, #3061 ) ;
#18416=DIRECTION ( 'NONE',  ( -5.626130192357176673E-16, -1.831515347669941892E-30, 1.000000000000000000 ) ) ;
#18439=CIRCLE ( 'NONE', #16064, 4.200000000000001954 ) ;
#18446=CARTESIAN_POINT ( 'NONE',  ( 2.463659247115867590, 38.82793883177424732, 91.78246379782397923 ) ) ;
#18459=CARTESIAN_POINT ( 'NONE',  ( 2.475532831258718591, 39.44063218796383552, 95.05433879953096721 ) ) ;
#18462=VERTEX_POINT ( 'NONE', #6227 ) ;
#18511=CARTESIAN_POINT ( 'NONE',  ( 0.5221537403065006355, 44.16218137147969003, 92.45433879953097289 ) ) ;
#18519=DIRECTION ( 'NONE',  ( -5.626130192357176673E-16, -1.831515347669941892E-30, 1.000000000000000000 ) ) ;
#18536=CARTESIAN_POINT ( 'NONE',  ( 5.666884522201895535, 41.76315400873614436, 93.18871379782397923 ) ) ;
#18544=FACE_OUTER_BOUND ( 'NONE', #3330, .T. ) ;
#18546=ORIENTED_EDGE ( 'NONE', *, *, #1842, .T. ) ;
#18551=CARTESIAN_POINT ( 'NONE',  ( 2.921181103050039418, 49.30691215337508737, 92.25121379782397923 ) ) ;
#18566=FACE_BOUND ( 'NONE', #4770, .T. ) ;
#18594=CARTESIAN_POINT ( 'NONE',  ( -2.313335635445064931, 37.76218137147968434, 95.05433879953096721 ) ) ;
#18639=CARTESIAN_POINT ( 'NONE',  ( 2.463659247115867146, 38.82793883177424732, 93.03246379782397923 ) ) ;
#18641=CARTESIAN_POINT ( 'NONE',  ( -1.187946976321872850, 48.86064447540922373, 94.36058879953097289 ) ) ;
#18654=CARTESIAN_POINT ( 'NONE',  ( -4.812088799398940075, 42.22067586467031930, 93.96996379782397923 ) ) ;
#18664=CARTESIAN_POINT ( 'NONE',  ( 5.856396280011939126, 46.10368687828906076, 94.43871379782397923 ) ) ;
#18673=CARTESIAN_POINT ( 'NONE',  ( -0.2740250116460755114, 39.09885644656073111, 92.45433879953098710 ) ) ;
#18700=CARTESIAN_POINT ( 'NONE',  ( -4.884656273474449861, 44.39824779480852612, 90.84496379953097289 ) ) ;
#18713=ORIENTED_EDGE ( 'NONE', *, *, #20758, .F. ) ;
#18752=CARTESIAN_POINT ( 'NONE',  ( -1.419351766502868761, 49.49642391118513274, 94.90746379782397923 ) ) ;
#18760=CARTESIAN_POINT ( 'NONE',  ( 6.660594192354429843, 43.89417127335556046, 93.11058879782397923 ) ) ;
#18762=CARTESIAN_POINT ( 'NONE',  ( 3.052272305227448967, 39.76218035589567990, 95.01850678128215577 ) ) ;
#18770=AXIS2_PLACEMENT_3D ( 'NONE', #7446, #2345, #18519 ) ;
#18775=ADVANCED_FACE ( 'NONE', ( #11227 ), #16113, .F. ) ;
#18789=CARTESIAN_POINT ( 'NONE',  ( -5.048451936153556474, 43.75436344969243407, 92.45433879953098710 ) ) ;
#18796=EDGE_CURVE ( 'NONE', #3932, #12110, #16041, .T. ) ;
#18803=CARTESIAN_POINT ( 'NONE',  ( 0.5221537403064959726, 50.56218137147968861, 95.05433879953096721 ) ) ;
#18850=CARTESIAN_POINT ( 'NONE',  ( -5.616286711741429905, 44.43019146960381960, 92.64183879782400766 ) ) ;
#18867=CARTESIAN_POINT ( 'NONE',  ( 4.666303754810079418, 40.22630141247467606, 95.62484283304920041 ) ) ;
#18872=ORIENTED_EDGE ( 'NONE', *, *, #14327, .F. ) ;
#18882=CARTESIAN_POINT ( 'NONE',  ( -5.199045795788149071, 43.94855844323328853, 95.05433879953095300 ) ) ;
#18890=CARTESIAN_POINT ( 'NONE',  ( 1.456841371642047411, 39.25032235153333460, 92.45433879953097289 ) ) ;
#18892=CARTESIAN_POINT ( 'NONE',  ( -4.812088799398940075, 42.22067586467031930, 93.96996379782397923 ) ) ;
#18910=FACE_OUTER_BOUND ( 'NONE', #12159, .T. ) ;
#18926=EDGE_CURVE ( 'NONE', #12946, #17868, #3318, .T. ) ;
#18955=FACE_OUTER_BOUND ( 'NONE', #11685, .T. ) ;
#18981=CARTESIAN_POINT ( 'NONE',  ( 0.5221537403065079630, 49.16218137147969003, 93.97886871425482980 ) ) ;
#18990=CARTESIAN_POINT ( 'NONE',  ( 0.6003407026341696096, 39.08370886253464960, 92.45433879953100131 ) ) ;
#18993=CARTESIAN_POINT ( 'NONE',  ( 0.2541436421823717318, 38.02374091943176637, 91.70433879782397923 ) ) ;
#19015=CARTESIAN_POINT ( 'NONE',  ( -3.134114116279071549, 48.15229756555780227, 90.68871379953098710 ) ) ;
#19028=CARTESIAN_POINT ( 'NONE',  ( 0.5221537403065015237, 49.16218137147969003, 92.72886871425484401 ) ) ;
#19048=LINE ( 'NONE', #1593, #11610 ) ;
#19053=DIRECTION ( 'NONE',  ( -1.301042606982606060E-16, -1.000000000000000000, 0.000000000000000000 ) ) ;
#19091=CARTESIAN_POINT ( 'NONE',  ( 5.052198367669452850, 48.31320248322254685, 94.51683879782399345 ) ) ;
#19099=CARTESIAN_POINT ( 'NONE',  ( -4.721961219230297324, 42.48895494285373786, 92.45433879953101552 ) ) ;
#19102=CARTESIAN_POINT ( 'NONE',  ( 2.463659247115866258, 38.82793883177424732, 94.28246379782397923 ) ) ;
#19134=DIRECTION ( 'NONE',  ( -2.775557561562892929E-15, -1.000000000000000000, 0.000000000000000000 ) ) ;
#19169=LINE ( 'NONE', #12482, #14546 ) ;
#19181=EDGE_CURVE ( 'NONE', #11953, #14920, #17251, .T. ) ;
#19187=DIRECTION ( 'NONE',  ( -5.626130192357176673E-16, -1.831515347669941892E-30, 1.000000000000000000 ) ) ;
#19195=CARTESIAN_POINT ( 'NONE',  ( -4.007890887056451135, 40.01116025973682611, 92.79808879782397923 ) ) ;
#19203=CARTESIAN_POINT ( 'NONE',  ( 1.853156886157175220, 39.32573803590444328, 92.47037068331223963 ) ) ;
#19217=CARTESIAN_POINT ( 'NONE',  ( 0.7582201636353277374, 49.56899138526064519, 94.28246379953097289 ) ) ;
#19229=ORIENTED_EDGE ( 'NONE', *, *, #14698, .F. ) ;
#19244=CARTESIAN_POINT ( 'NONE',  ( -5.044287576081563529, 45.27497882680665242, 92.45433879953097289 ) ) ;
#19253=ORIENTED_EDGE ( 'NONE', *, *, #15742, .T. ) ;
#19275=( GEOMETRIC_REPRESENTATION_CONTEXT ( 3 ) GLOBAL_UNCERTAINTY_ASSIGNED_CONTEXT ( ( #15131 ) ) GLOBAL_UNIT_ASSIGNED_CONTEXT ( ( #93, #16168, #3384 ) ) REPRESENTATION_CONTEXT ( 'NONE', 'WORKASPACE' ) );
#19285=VECTOR ( 'NONE', #266, 1000.000000000000000 ) ;
#19296=CARTESIAN_POINT ( 'NONE',  ( -3.628867371436363953, 48.69222599884265179, 93.73558879782397923 ) ) ;
#19297=CARTESIAN_POINT ( 'NONE',  ( -4.812088799398938299, 42.22067586467031930, 91.31371379782397923 ) ) ;
#19308=EDGE_LOOP ( 'NONE', ( #13873, #7059, #19544, #12757, #3203, #15262, #18713, #14477 ) ) ;
#19317=CARTESIAN_POINT ( 'NONE',  ( -3.134114116279072881, 48.15229756555780227, 94.43871379953097289 ) ) ;
#19344=CARTESIAN_POINT ( 'NONE',  ( -4.812088799398939187, 42.22067586467031930, 92.56371379782397923 ) ) ;
#19351=( BOUNDED_SURFACE ( )  B_SPLINE_SURFACE ( 1, 2, ( 
 ( #1543, #4710, #15816, #17400, #4406, #6009, #2825, #11238, #7618, #18993, #20882, #16123, #14000, #17710, #7823, #2925, #9537, #6111, #12615, #3142, #1335, #6312, #9329, #19195, #12813, #14412, #10829, #7717, #11130, #14199, #16020, #14100, #20483, #5916, #9643, #19296, #9425, #12413, #18892, #4302, #11030, #20583, #19102, #17501, #4610, #1130, #17292, #2718, #10929, #9225, #17600, #15711, #12509, #3028, #15914, #1228, #20677, #12717, #4512, #6217, #14306 ),
 ( #20783, #1440, #7925, #19818, #9843, #11442, #19509, #48, #17914, #5240, #1647, #13033, #14929, #10162, #16644, #11756, #1860, #18023, #3552, #148, #6630, #18230, #16441, #351, #3337, #13238, #6840, #8447, #4822, #1760, #5134, #8242, #10056, #8130, #14515, #8028, #3650, #13347, #3444, #20981, #6415, #12924, #5028, #14622, #13131, #9741, #19403, #9958, #6734, #8345, #11344, #17813, #3238, #16222, #6527, #4921, #16331, #14727, #19716, #19606, #11547 ) ),
 .UNSPECIFIED., .F., .F., .F. ) 
 B_SPLINE_SURFACE_WITH_KNOTS ( ( 2, 2 ),
 ( 3, 2, 2, 2, 2, 2, 2, 2, 2, 2, 2, 2, 2, 2, 2, 2, 2, 2, 2, 2, 2, 2, 2, 2, 2, 2, 2, 2, 2, 2, 3 ),
 ( 0.000000000000000000, 1.000000000000000000 ),
 ( 0.000000000000000000, 0.03125000000000000000, 0.06250000000000000000, 0.09375000000000000000, 0.1250000000000000000, 0.1562500000000000000, 0.1875000000000000000, 0.2187500000000000000, 0.2500000000000000000, 0.2812500000000000000, 0.3125000000000000000, 0.3437500000000000000, 0.3750000000000000000, 0.4062500000000000000, 0.4375000000000000000, 0.4687500000000000000, 0.5000000000000000000, 0.5312500000000000000, 0.5625000000000000000, 0.5937500000000000000, 0.6250000000000000000, 0.6562500000000000000, 0.6875000000000000000, 0.7187500000000000000, 0.7500000000000000000, 0.7812500000000000000, 0.8125000000000000000, 0.8437500000000000000, 0.8750000000000000000, 0.9062500000000000000, 0.9200238603477419730 ),
 .UNSPECIFIED. ) 
 GEOMETRIC_REPRESENTATION_ITEM ( )  RATIONAL_B_SPLINE_SURFACE ( (
 ( 1.000000000000000000, 0.9238795325112867385, 1.000000000000000000, 0.9238795325112867385, 1.000000000000000000, 0.9238795325112867385, 1.000000000000000000, 0.9238795325112867385, 1.000000000000000000, 0.9238795325112867385, 1.000000000000000000, 0.9238795325112867385, 1.000000000000000000, 0.9238795325112867385, 1.000000000000000000, 0.9238795325112867385, 1.000000000000000000, 0.9238795325112867385, 1.000000000000000000, 0.9238795325112867385, 1.000000000000000000, 0.9238795325112867385, 1.000000000000000000, 0.9238795325112867385, 1.000000000000000000, 0.9238795325112867385, 1.000000000000000000, 0.9238795325112867385, 1.000000000000000000, 0.9238795325112867385, 1.000000000000000000, 0.9238795325112867385, 1.000000000000000000, 0.9238795325112867385, 1.000000000000000000, 0.9238795325112867385, 1.000000000000000000, 0.9238795325112867385, 1.000000000000000000, 0.9238795325112867385, 1.000000000000000000, 0.9238795325112867385, 1.000000000000000000, 0.9238795325112867385, 1.000000000000000000, 0.9238795325112867385, 1.000000000000000000, 0.9238795325112867385, 1.000000000000000000, 0.9238795325112867385, 1.000000000000000000, 0.9238795325112867385, 1.000000000000000000, 0.9238795325112867385, 1.000000000000000000, 0.9238795325112867385, 1.000000000000000000, 0.9238795325112867385, 1.000000000000000000, 0.9664488739585801458, 0.9624739734918166256),
 ( 1.000000000000000000, 0.9238795325112867385, 1.000000000000000000, 0.9238795325112867385, 1.000000000000000000, 0.9238795325112867385, 1.000000000000000000, 0.9238795325112867385, 1.000000000000000000, 0.9238795325112867385, 1.000000000000000000, 0.9238795325112867385, 1.000000000000000000, 0.9238795325112867385, 1.000000000000000000, 0.9238795325112867385, 1.000000000000000000, 0.9238795325112867385, 1.000000000000000000, 0.9238795325112867385, 1.000000000000000000, 0.9238795325112867385, 1.000000000000000000, 0.9238795325112867385, 1.000000000000000000, 0.9238795325112867385, 1.000000000000000000, 0.9238795325112867385, 1.000000000000000000, 0.9238795325112867385, 1.000000000000000000, 0.9238795325112867385, 1.000000000000000000, 0.9238795325112867385, 1.000000000000000000, 0.9238795325112867385, 1.000000000000000000, 0.9238795325112867385, 1.000000000000000000, 0.9238795325112867385, 1.000000000000000000, 0.9238795325112867385, 1.000000000000000000, 0.9238795325112867385, 1.000000000000000000, 0.9238795325112867385, 1.000000000000000000, 0.9238795325112867385, 1.000000000000000000, 0.9238795325112867385, 1.000000000000000000, 0.9238795325112867385, 1.000000000000000000, 0.9238795325112867385, 1.000000000000000000, 0.9238795325112867385, 1.000000000000000000, 0.9238795325112867385, 1.000000000000000000, 0.9664488739585801458, 0.9624739734918166256) ) ) 
 REPRESENTATION_ITEM ( '' )  SURFACE ( )  );
#19369=CARTESIAN_POINT ( 'NONE',  ( 5.381183826744221577, 45.53750893733308658, 92.45433879953098710 ) ) ;
#19383=ADVANCED_FACE ( 'NONE', ( #960 ), #8950, .F. ) ;
#19397=CYLINDRICAL_SURFACE ( 'NONE', #18005, 4.200000000000001954 ) ;
#19403=CARTESIAN_POINT ( 'NONE',  ( 5.220616844236030119, 45.87228208810806507, 94.98558879611698558 ) ) ;
#19404=CARTESIAN_POINT ( 'NONE',  ( 4.673174852049363004, 39.63213674411673537, 91.70433879782397923 ) ) ;
#19429=CARTESIAN_POINT ( 'NONE',  ( 5.053692675489762642, 42.04909006277621586, 92.64183879953097289 ) ) ;
#19454=CARTESIAN_POINT ( 'NONE',  ( -1.419351766502867873, 49.49642391118513274, 93.50121379782397923 ) ) ;
#19504=CARTESIAN_POINT ( 'NONE',  ( 1.528832406012765377, 49.31710775539747260, 95.05433879953095300 ) ) ;
#19509=CARTESIAN_POINT ( 'NONE',  ( -4.176309363623029292, 42.45208065485131499, 91.86058879611698558 ) ) ;
#19526=CARTESIAN_POINT ( 'NONE',  ( 0.5221537403064999694, 39.16218137147969003, 92.45433879953097289 ) ) ;
#19532=CARTESIAN_POINT ( 'NONE',  ( 2.635245049009969254, 48.69372030666295359, 92.95433879953098710 ) ) ;
#19544=ORIENTED_EDGE ( 'NONE', *, *, #10554, .F. ) ;
#19547=DIRECTION ( 'NONE',  ( 1.193617070626243237E-16, 1.000000000000000000, 1.876284981264363171E-30 ) ) ;
#19556=PRODUCT_DEFINITION_SHAPE ( 'NONE', 'NONE',  #16133 ) ;
#19592=ORIENTED_EDGE ( 'NONE', *, *, #15429, .T. ) ;
#19606=CARTESIAN_POINT ( 'NONE',  ( 3.052270314075706814, 39.76217963117571230, 95.95600669793734028 ) ) ;
#19607=CARTESIAN_POINT ( 'NONE',  ( 2.463659247115867146, 38.82793883177424732, 92.87621379782399345 ) ) ;
#19611=EDGE_CURVE ( 'NONE', #10155, #12110, #19048, .T. ) ;
#19633=CARTESIAN_POINT ( 'NONE',  ( -4.176309363623030180, 42.45208065485131499, 93.42308879953097289 ) ) ;
#19659=CARTESIAN_POINT ( 'NONE',  ( 0.7901638384306272078, 50.30062182352762079, 94.67308879782399345 ) ) ;
#19716=CARTESIAN_POINT ( 'NONE',  ( 2.232254456934870124, 39.46371826755015633, 95.92308879611699979 ) ) ;
#19718=CARTESIAN_POINT ( 'NONE',  ( -3.628867371436363509, 48.69222599884265179, 92.32933879782399345 ) ) ;
#19756=DIRECTION ( 'NONE',  ( 1.290716872006552287E-16, 1.000000000000000000, 0.000000000000000000 ) ) ;
#19761=SURFACE_STYLE_FILL_AREA ( #3186 ) ;
#19811=CARTESIAN_POINT ( 'NONE',  ( 0.5221537403065048544, 39.16218137147969003, 93.66636871766883132 ) ) ;
#19818=CARTESIAN_POINT ( 'NONE',  ( -3.134114116279071549, 48.15229756555780227, 91.62621379611699979 ) ) ;
#19819=CARTESIAN_POINT ( 'NONE',  ( 0.2541436421823710656, 38.02374091943176637, 92.95433879782399345 ) ) ;
#19826=ORIENTED_EDGE ( 'NONE', *, *, #15206, .T. ) ;
#19861=ADVANCED_FACE ( 'NONE', ( #7091 ), #20182, .F. ) ;
#19896=PRODUCT ( 'Bushing', 'Bushing', '', ( #7295 ) ) ;
#19905=ORIENTED_EDGE ( 'NONE', *, *, #603, .F. ) ;
#19911=CARTESIAN_POINT ( 'NONE',  ( -1.590937568396969759, 39.63064243629642647, 93.57933879953097289 ) ) ;
#19919=CARTESIAN_POINT ( 'NONE',  ( 6.660594192354429843, 43.89417127335556046, 93.26683879782399345 ) ) ;
#19938=ORIENTED_EDGE ( 'NONE', *, *, #19611, .T. ) ;
#19980=CARTESIAN_POINT ( 'NONE',  ( 0.5221537403065006355, 48.36218137147969287, 92.45433879953097289 ) ) ;
#19981=ADVANCED_BREP_SHAPE_REPRESENTATION ( '', ( #11462, #18366 ), #17679 ) ;
#20021=CARTESIAN_POINT ( 'NONE',  ( 0.7901638384306272078, 50.30062182352762079, 94.67308879782399345 ) ) ;
#20041=CARTESIAN_POINT ( 'NONE',  ( 0.5819204035424812016, 38.92295143466739660, 95.05433879953096721 ) ) ;
#20055=CARTESIAN_POINT ( 'NONE',  ( 4.512269934384612213, 47.81844922806527620, 94.12621379953098710 ) ) ;
#20083=EDGE_LOOP ( 'NONE', ( #9971, #17355, #7936, #8460 ) ) ;
#20133=CARTESIAN_POINT ( 'NONE',  ( -5.616286711741430793, 44.43019146960381960, 93.89183879782397923 ) ) ;
#20148=CARTESIAN_POINT ( 'NONE',  ( -4.746143138089100155, 42.07168972858362821, 95.05433879953095300 ) ) ;
#20149=FACE_OUTER_BOUND ( 'NONE', #14720, .T. ) ;
#20165=EDGE_LOOP ( 'NONE', ( #16437, #14223, #12031, #20732 ) ) ;
#20168=ORIENTED_EDGE ( 'NONE', *, *, #8088, .F. ) ;
#20182=PLANE ( 'NONE',  #9616 ) ;
#20217=CARTESIAN_POINT ( 'NONE',  ( 5.052198367669452850, 48.31320248322255395, 94.67308879782399345 ) ) ;
#20234=CARTESIAN_POINT ( 'NONE',  ( -5.616286711741430793, 44.43019146960381960, 94.98558879782399345 ) ) ;
#20248=CARTESIAN_POINT ( 'NONE',  ( -4.178163250680730023, 41.13787398766260139, 95.05433879953092458 ) ) ;
#20256=EDGE_CURVE ( 'NONE', #1086, #11013, #3674, .T. ) ;
#20277=( BOUNDED_CURVE ( )  B_SPLINE_CURVE ( 2, ( #11109, #14701, #9508, #4686, #1736, #6497, #6709, #12790, #124 ),
 .UNSPECIFIED., .F., .F. ) 
 B_SPLINE_CURVE_WITH_KNOTS ( ( 3, 2, 2, 2, 3 ),
 ( 0.6423390146554854852, 0.6562500000000000000, 0.6875000000000000000, 0.7187500000000000000, 0.7325704129817647292 ),
 .UNSPECIFIED. ) 
 CURVE ( )  GEOMETRIC_REPRESENTATION_ITEM ( )  RATIONAL_B_SPLINE_CURVE ( ( 0.9623977609649205789, 0.9661148573551012753, 1.000000000000000000, 0.9238795325112867385, 1.000000000000000000, 0.9238795325112867385, 1.000000000000000000, 0.9663354784941116105, 0.9624474427510953944 ) ) 
 REPRESENTATION_ITEM ( '' )  );
#20278=CARTESIAN_POINT ( 'NONE',  ( 0.5221537403065015237, 48.36218137147969287, 92.45433879953097289 ) ) ;
#20279=CARTESIAN_POINT ( 'NONE',  ( -4.009385194876760927, 46.27527268018315709, 90.76683879953097289 ) ) ;
#20338=CARTESIAN_POINT ( 'NONE',  ( 1.403788643848841389, 39.16218137147969003, 94.95233169107483207 ) ) ;
#20344=CARTESIAN_POINT ( 'NONE',  ( 3.394633603133437205, 39.16678578622979501, 95.56538158822176854 ) ) ;
#20357=CARTESIAN_POINT ( 'NONE',  ( 2.921181103050038086, 49.30691215337508737, 94.59496379782397923 ) ) ;
#20367=CARTESIAN_POINT ( 'NONE',  ( -3.063797695301091473, 40.22636611860890810, 92.45433879953094447 ) ) ;
#20390=B_SPLINE_CURVE_WITH_KNOTS ( 'NONE', 3,
 ( #7634, #9241, #14014, #17205, #2630, #9130 ),
 .UNSPECIFIED., .F., .F.,
 ( 4, 2, 4 ),
 ( 0.000000000000000000, 0.002233127396118993191, 0.004466254792237986382 ),
 .UNSPECIFIED. ) ;
#20452=CARTESIAN_POINT ( 'NONE',  ( 2.921181103050038974, 49.30691215337508737, 93.34496379782397923 ) ) ;
#20458=AXIS2_PLACEMENT_3D ( 'NONE', #2954, #20611, #19134 ) ;
#20459=CARTESIAN_POINT ( 'NONE',  ( 5.176818351154000020, 40.65164613849449182, 95.64871367200940711 ) ) ;
#20483=CARTESIAN_POINT ( 'NONE',  ( 2.921181103050038530, 49.30691215337508737, 93.50121379782399345 ) ) ;
#20491=VERTEX_POINT ( 'NONE', #3025 ) ;
#20546=CARTESIAN_POINT ( 'NONE',  ( 0.7901638384306272078, 50.30062182352762079, 94.82933879782399345 ) ) ;
#20560=CARTESIAN_POINT ( 'NONE',  ( 2.463659247115865369, 38.82793883177424732, 95.53246379782397923 ) ) ;
#20568=CARTESIAN_POINT ( 'NONE',  ( 3.357643116058060428, 37.76218137147968434, 96.05433879953096721 ) ) ;
#20577=DIRECTION ( 'NONE',  ( -5.626130192357176673E-16, -1.831515347669941892E-30, 1.000000000000000000 ) ) ;
#20583=CARTESIAN_POINT ( 'NONE',  ( 0.2541436421823703440, 38.02374091943176637, 94.20433879782400766 ) ) ;
#20611=DIRECTION ( 'NONE',  ( 5.626130192357176673E-16, 1.831515347669941892E-30, -1.000000000000000000 ) ) ;
#20633=CARTESIAN_POINT ( 'NONE',  ( 0.5221537403064990812, 39.96218137147968719, 96.05433879953096721 ) ) ;
#20640=CARTESIAN_POINT ( 'NONE',  ( 4.673174852049362116, 39.63213674411673537, 93.11058879782397923 ) ) ;
#20663=EDGE_CURVE ( 'NONE', #10333, #1086, #16826, .T. ) ;
#20673=CARTESIAN_POINT ( 'NONE',  ( -3.711822497969910817, 40.81753442731484682, 92.45433879953094447 ) ) ;
#20676=AXIS2_PLACEMENT_3D ( 'NONE', #16968, #11121, #1428 ) ;
#20677=CARTESIAN_POINT ( 'NONE',  ( -1.876873622437040590, 39.01745058958429269, 95.37621379782397923 ) ) ;
#20732=ORIENTED_EDGE ( 'NONE', *, *, #20903, .F. ) ;
#20752=ORIENTED_EDGE ( 'NONE', *, *, #15366, .F. ) ;
#20758=EDGE_CURVE ( 'NONE', #13884, #3900, #9180, .T. ) ;
#20759=AXIS2_PLACEMENT_3D ( 'NONE', #18065, #13173, #19547 ) ;
#20769=CARTESIAN_POINT ( 'NONE',  ( -5.121096889713498079, 43.19689566777418577, 95.05433879953096721 ) ) ;
#20783=CARTESIAN_POINT ( 'NONE',  ( 2.635245049009970142, 48.69372030666295359, 91.39183879611699979 ) ) ;
#20790=ADVANCED_FACE ( 'NONE', ( #4350 ), #2775, .T. ) ;
#20810=CARTESIAN_POINT ( 'NONE',  ( 0.2860873169776696479, 38.75537135769874197, 94.90746379953098710 ) ) ;
#20829=CIRCLE ( 'NONE', #105, 4.200000000000001954 ) ;
#20839=( BOUNDED_CURVE ( )  B_SPLINE_CURVE ( 2, ( #12170, #20338, #12282, #18762, #15151 ),
 .UNSPECIFIED., .F., .F. ) 
 B_SPLINE_CURVE_WITH_KNOTS ( ( 3, 2, 3 ),
 ( 0.8923390146554854852, 0.9062500000000000000, 0.9200238926711118426 ),
 .UNSPECIFIED. ) 
 CURVE ( )  GEOMETRIC_REPRESENTATION_ITEM ( )  RATIONAL_B_SPLINE_CURVE ( ( 0.9623977609649205789, 0.9661148573551012753, 1.000000000000000000, 0.9664487952235394363, 0.9624739548360365937 ) ) 
 REPRESENTATION_ITEM ( '' )  );
#20853=CARTESIAN_POINT ( 'NONE',  ( 3.889041150776882727, 48.17793082961422613, 92.45433879953097289 ) ) ;
#20882=CARTESIAN_POINT ( 'NONE',  ( 2.463659247115867590, 38.82793883177424732, 91.78246379782397923 ) ) ;
#20903=EDGE_CURVE ( 'NONE', #9268, #17689, #411, .T. ) ;
#20905=CARTESIAN_POINT ( 'NONE',  ( 4.178421596892071044, 40.17206517740157778, 92.56371379953098710 ) ) ;
#20949=CARTESIAN_POINT ( 'NONE',  ( 5.269956278383879145, 45.96059190786396442, 92.45433879953094447 ) ) ;
#20975=CARTESIAN_POINT ( 'NONE',  ( 0.5221537403065006355, 44.16218137147969003, 92.45433879953097289 ) ) ;
#20978=CARTESIAN_POINT ( 'NONE',  ( 0.2343434307403843286, 49.48026920881595458, 95.05433879953099563 ) ) ;
#20981=CARTESIAN_POINT ( 'NONE',  ( -3.467962453771612275, 40.50591351489412517, 94.43871379611699979 ) ) ;
#20982=CARTESIAN_POINT ( 'NONE',  ( 5.666884522201895535, 41.76315400873614436, 93.03246379782397923 ) ) ;
#20987=ORIENTED_EDGE ( 'NONE', *, *, #7405, .F. ) ;
#20995=FACE_OUTER_BOUND ( 'NONE', #5278, .T. ) ;
#20998=ORIENTED_EDGE ( 'NONE', *, *, #8088, .T. ) ;
#21005=CARTESIAN_POINT ( 'NONE',  ( -3.134114116279072881, 48.15229756555780227, 93.18871379953097289 ) ) ;
#21023=FACE_OUTER_BOUND ( 'NONE', #9452, .T. ) ;
ENDSEC;
END-ISO-10303-21;
